ISO-10303-21;
HEADER;
FILE_DESCRIPTION (('STEP AP214'),
    '1' );
FILE_NAME ('taper roller bearing_iso_ISO 355-2 - 2BD25 - 22,SI,NC,22.step',
    '2026-09-30T12:41:04',
    ( '' ),
    ( '' ),
    'SwSTEP 2.0',
    'SolidWorks 2026',
    '' );
FILE_SCHEMA (( 'AUTOMOTIVE_DESIGN' ));
ENDSEC;

DATA;
#6=ORIENTED_EDGE ( 'NONE', *, *, #30386, .F. ) ;
#27=FACE_BOUND ( 'NONE', #47699, .T. ) ;
#266=EDGE_LOOP ( 'NONE', ( #6, #16108, #6404, #41831 ) ) ;
#278=CIRCLE ( 'NONE', #3373, 13.90444123027096879 ) ;
#372=AXIS2_PLACEMENT_3D ( 'NONE', #44697, #34162, #22185 ) ;
#548=CIRCLE ( 'NONE', #12256, 20.99999999999999645 ) ;
#557=VECTOR ( 'NONE', #31928, 1000.000000000000000 ) ;
#633=DIRECTION ( 'NONE',  ( 1.000000000000000000, 0.000000000000000000, 0.000000000000000000 ) ) ;
#714=AXIS2_PLACEMENT_3D ( 'NONE', #45123, #37045, #11592 ) ;
#768=EDGE_CURVE ( 'NONE', #35835, #19346, #17395, .T. ) ;
#777=ORIENTED_EDGE ( 'NONE', *, *, #41476, .T. ) ;
#780=SHAPE_DEFINITION_REPRESENTATION ( #5794, #22809 ) ;
#799=CYLINDRICAL_SURFACE ( 'NONE', #46893, 20.99999999999999645 ) ;
#804=ORIENTED_EDGE ( 'NONE', *, *, #24709, .F. ) ;
#818=DIRECTION ( 'NONE',  ( 0.000000000000000000, 0.000000000000000000, -1.000000000000000000 ) ) ;
#1002=DIRECTION ( 'NONE',  ( -1.000000000000000000, -0.000000000000000000, -0.000000000000000000 ) ) ;
#1024=CIRCLE ( 'NONE', #13552, 0.2999999999999981570 ) ;
#1041=DIRECTION ( 'NONE',  ( 1.000000000000000000, 0.000000000000000000, 0.000000000000000000 ) ) ;
#1052=CIRCLE ( 'NONE', #10463, 19.05560546998412974 ) ;
#1062=DIRECTION ( 'NONE',  ( 1.000000000000000000, 0.000000000000000000, 0.000000000000000000 ) ) ;
#1099=CARTESIAN_POINT ( 'NONE',  ( -10.90093335751250692, 0.000000000000000000, 0.000000000000000000 ) ) ;
#1237=CARTESIAN_POINT ( 'NONE',  ( -2.977765906491215642, 0.000000000000000000, -15.39727592589476579 ) ) ;
#1272=CARTESIAN_POINT ( 'NONE',  ( -2.981742216678212820, 0.000000000000000000, 15.39727592608509177 ) ) ;
#1273=( LENGTH_UNIT ( ) NAMED_UNIT ( * ) SI_UNIT ( .MILLI., .METRE. ) );
#1280=ORIENTED_EDGE ( 'NONE', *, *, #21742, .F. ) ;
#1433=ORIENTED_EDGE ( 'NONE', *, *, #32119, .T. ) ;
#1440=ORIENTED_EDGE ( 'NONE', *, *, #24709, .T. ) ;
#1461=ORIENTED_EDGE ( 'NONE', *, *, #27036, .T. ) ;
#1467=CARTESIAN_POINT ( 'NONE',  ( 6.938893903907228378E-15, 0.000000000000000000, 0.000000000000000000 ) ) ;
#1510=PRESENTATION_STYLE_ASSIGNMENT (( #42637 ) ) ;
#1617=EDGE_LOOP ( 'NONE', ( #30678, #1433, #17533, #44944 ) ) ;
#1685=CARTESIAN_POINT ( 'NONE',  ( -10.90473778262209414, 0.000000000000000000, -13.71319123046128752 ) ) ;
#1704=EDGE_CURVE ( 'NONE', #3678, #34848, #8034, .T. ) ;
#1706=VERTEX_POINT ( 'NONE', #20558 ) ;
#1860=CARTESIAN_POINT ( 'NONE',  ( -42.50000000000000000, 0.000000000000000000, 0.000000000000000000 ) ) ;
#1870=CARTESIAN_POINT ( 'NONE',  ( -0.2999999999999964362, 1.567547902908612184E-15, 12.80000000000000071 ) ) ;
#1880=AXIS2_PLACEMENT_3D ( 'NONE', #27810, #9662, #31479 ) ;
#1941=CARTESIAN_POINT ( 'NONE',  ( -0.2999999999999964362, 0.000000000000000000, 0.000000000000000000 ) ) ;
#1957=EDGE_CURVE ( 'NONE', #13671, #29705, #10340, .T. ) ;
#2026=AXIS2_PLACEMENT_3D ( 'NONE', #35725, #43556, #46755 ) ;
#2052=LINE ( 'NONE', #32147, #7095 ) ;
#2109=LINE ( 'NONE', #47126, #34666 ) ;
#2123=AXIS2_PLACEMENT_3D ( 'NONE', #48325, #30225, #33404 ) ;
#2235=LINE ( 'NONE', #32114, #33592 ) ;
#2259=ORIENTED_EDGE ( 'NONE', *, *, #8192, .F. ) ;
#2347=CARTESIAN_POINT ( 'NONE',  ( -10.90473778262209414, 1.679381574647996852E-15, 13.71319123046128752 ) ) ;
#2391=ORIENTED_EDGE ( 'NONE', *, *, #33210, .F. ) ;
#2404=CONICAL_SURFACE ( 'NONE', #37611, 15.39727592608509177, 1.361356816555577609 ) ;
#2437=LINE ( 'NONE', #21045, #35509 ) ;
#2561=ORIENTED_EDGE ( 'NONE', *, *, #33033, .F. ) ;
#2604=DIRECTION ( 'NONE',  ( 0.000000000000000000, 0.000000000000000000, -1.000000000000000000 ) ) ;
#2630=( LENGTH_UNIT ( ) NAMED_UNIT ( * ) SI_UNIT ( .MILLI., .METRE. ) );
#2632=VECTOR ( 'NONE', #12078, 1000.000000000000114 ) ;
#2646=AXIS2_PLACEMENT_3D ( 'NONE', #23223, #37185, #38156 ) ;
#2697=ORIENTED_EDGE ( 'NONE', *, *, #37434, .F. ) ;
#2730=ADVANCED_FACE ( 'NONE', ( #22392 ), #46678, .T. ) ;
#2744=DIRECTION ( 'NONE',  ( 1.000000000000000000, 0.000000000000000000, 0.000000000000000000 ) ) ;
#2776=CIRCLE ( 'NONE', #30158, 13.90444123027096879 ) ;
#2781=DIRECTION ( 'NONE',  ( 1.000000000000000000, 0.000000000000000000, 0.000000000000000000 ) ) ;
#2807=CARTESIAN_POINT ( 'NONE',  ( -3.000000000000002665, 0.000000000000000000, 0.000000000000000000 ) ) ;
#2893=CARTESIAN_POINT ( 'NONE',  ( -0.2999999999999947153, 1.530808498934191521E-15, 12.50000000000000000 ) ) ;
#2917=DIRECTION ( 'NONE',  ( 1.000000000000000000, 0.000000000000000000, 0.000000000000000000 ) ) ;
#2952=( GEOMETRIC_REPRESENTATION_CONTEXT ( 3 ) GLOBAL_UNCERTAINTY_ASSIGNED_CONTEXT ( ( #14457 ) ) GLOBAL_UNIT_ASSIGNED_CONTEXT ( ( #13192, #28117, #17094 ) ) REPRESENTATION_CONTEXT ( 'NONE', 'WORKASPACE' ) );
#3031=EDGE_LOOP ( 'NONE', ( #23909, #3426, #11098, #27878 ) ) ;
#3036=DIRECTION ( 'NONE',  ( 0.000000000000000000, 0.000000000000000000, -1.000000000000000000 ) ) ;
#3054=ADVANCED_FACE ( 'NONE', ( #10599, #5973 ), #21352, .T. ) ;
#3143=ORIENTED_EDGE ( 'NONE', *, *, #36549, .T. ) ;
#3209=ORIENTED_EDGE ( 'NONE', *, *, #21139, .T. ) ;
#3275=ORIENTED_EDGE ( 'NONE', *, *, #28327, .F. ) ;
#3293=AXIS2_PLACEMENT_3D ( 'NONE', #9939, #24864, #21901 ) ;
#3356=CIRCLE ( 'NONE', #23002, 19.05560546998412974 ) ;
#3373=AXIS2_PLACEMENT_3D ( 'NONE', #9987, #25151, #6097 ) ;
#3385=ORIENTED_EDGE ( 'NONE', *, *, #1957, .T. ) ;
#3426=ORIENTED_EDGE ( 'NONE', *, *, #13173, .F. ) ;
#3469=ORIENTED_EDGE ( 'NONE', *, *, #10515, .T. ) ;
#3485=CARTESIAN_POINT ( 'NONE',  ( -3.000000000000002665, 0.000000000000000000, 0.000000000000000000 ) ) ;
#3502=AXIS2_PLACEMENT_3D ( 'NONE', #30094, #30566, #38157 ) ;
#3547=CYLINDRICAL_SURFACE ( 'NONE', #33369, 13.90444123027096879 ) ;
#3574=DIRECTION ( 'NONE',  ( -1.000000000000000000, 0.000000000000000000, 0.000000000000000000 ) ) ;
#3609=EDGE_CURVE ( 'NONE', #19346, #14976, #8354, .T. ) ;
#3611=( NAMED_UNIT ( * ) SI_UNIT ( $, .STERADIAN. ) SOLID_ANGLE_UNIT ( ) );
#3624=ADVANCED_FACE ( 'NONE', ( #35870 ), #48214, .F. ) ;
#3667=DIRECTION ( 'NONE',  ( 1.000000000000000000, 0.000000000000000000, 0.000000000000000000 ) ) ;
#3670=ORIENTED_EDGE ( 'NONE', *, *, #32119, .F. ) ;
#3678=VERTEX_POINT ( 'NONE', #13598 ) ;
#3807=CARTESIAN_POINT ( 'NONE',  ( -3.000000000000002665, 0.000000000000000000, -19.21700905503013601 ) ) ;
#3890=CIRCLE ( 'NONE', #28136, 13.71319123027096865 ) ;
#3910=DIRECTION ( 'NONE',  ( 0.000000000000000000, 0.000000000000000000, 1.000000000000000000 ) ) ;
#4035=DIRECTION ( 'NONE',  ( 1.000000000000000000, 0.000000000000000000, 0.000000000000000000 ) ) ;
#4143=FACE_OUTER_BOUND ( 'NONE', #5628, .T. ) ;
#4144=EDGE_CURVE ( 'NONE', #23375, #48194, #9888, .T. ) ;
#4206=DIRECTION ( 'NONE',  ( -1.000000000000000000, 0.000000000000000000, -0.000000000000000000 ) ) ;
#4644=EDGE_CURVE ( 'NONE', #46875, #27937, #32165, .T. ) ;
#4646=ADVANCED_FACE ( 'NONE', ( #28382 ), #29769, .T. ) ;
#4766=ORIENTED_EDGE ( 'NONE', *, *, #19000, .F. ) ;
#4876=FACE_OUTER_BOUND ( 'NONE', #26450, .T. ) ;
#4924=DIRECTION ( 'NONE',  ( 0.000000000000000000, 0.000000000000000000, 1.000000000000000000 ) ) ;
#4931=FILL_AREA_STYLE ('',( #45556 ) ) ;
#4961=DIRECTION ( 'NONE',  ( 1.000000000000000000, -0.000000000000000000, -0.000000000000000000 ) ) ;
#5059=DIRECTION ( 'NONE',  ( -1.000000000000000000, 0.000000000000000000, 0.000000000000000000 ) ) ;
#5087=CARTESIAN_POINT ( 'NONE',  ( -42.50000000000000000, 0.000000000000000000, -13.90444123027096879 ) ) ;
#5129=PLANE ( 'NONE',  #32334 ) ;
#5152=EDGE_CURVE ( 'NONE', #13922, #22705, #7830, .T. ) ;
#5384=ADVANCED_FACE ( 'NONE', ( #12337 ), #44627, .F. ) ;
#5528=EDGE_CURVE ( 'NONE', #6365, #37954, #26641, .T. ) ;
#5597=EDGE_CURVE ( 'NONE', #44505, #13391, #22063, .T. ) ;
#5628=EDGE_LOOP ( 'NONE', ( #22431, #25233, #4766, #43478 ) ) ;
#5661=FACE_OUTER_BOUND ( 'NONE', #14431, .T. ) ;
#5724=EDGE_CURVE ( 'NONE', #20650, #8981, #22167, .T. ) ;
#5746=ORIENTED_EDGE ( 'NONE', *, *, #13295, .T. ) ;
#5794=PRODUCT_DEFINITION_SHAPE ( 'NONE', 'NONE',  #12192 ) ;
#5816=DIRECTION ( 'NONE',  ( 1.000000000000000000, 0.000000000000000000, 0.000000000000000000 ) ) ;
#5897=DIRECTION ( 'NONE',  ( 1.000000000000000000, 0.000000000000000000, 0.000000000000000000 ) ) ;
#5899=EDGE_LOOP ( 'NONE', ( #25906, #16174, #28832, #23449 ) ) ;
#5922=DIRECTION ( 'NONE',  ( 0.000000000000000000, 0.000000000000000000, -1.000000000000000000 ) ) ;
#5973=FACE_BOUND ( 'NONE', #25646, .T. ) ;
#6023=LINE ( 'NONE', #20941, #21247 ) ;
#6057=ORIENTED_EDGE ( 'NONE', *, *, #6163, .T. ) ;
#6082=ORIENTED_EDGE ( 'NONE', *, *, #24203, .T. ) ;
#6097=DIRECTION ( 'NONE',  ( 0.000000000000000000, 0.000000000000000000, 1.000000000000000000 ) ) ;
#6121=CARTESIAN_POINT ( 'NONE',  ( -42.50000000000000000, 0.000000000000000000, 0.000000000000000000 ) ) ;
#6163=EDGE_CURVE ( 'NONE', #30318, #14976, #22216, .T. ) ;
#6365=VERTEX_POINT ( 'NONE', #33693 ) ;
#6366=ORIENTED_EDGE ( 'NONE', *, *, #9945, .F. ) ;
#6404=ORIENTED_EDGE ( 'NONE', *, *, #40347, .T. ) ;
#6433=DIRECTION ( 'NONE',  ( 0.9781476007338069101, 0.000000000000000000, -0.2079116908177528755 ) ) ;
#6606=ORIENTED_EDGE ( 'NONE', *, *, #4144, .F. ) ;
#6619=DIRECTION ( 'NONE',  ( 0.000000000000000000, 0.000000000000000000, 1.000000000000000000 ) ) ;
#6640=ORIENTED_EDGE ( 'NONE', *, *, #23097, .T. ) ;
#6675=AXIS2_PLACEMENT_3D ( 'NONE', #24838, #17730, #47366 ) ;
#6920=FACE_OUTER_BOUND ( 'NONE', #7118, .T. ) ;
#6932=CARTESIAN_POINT ( 'NONE',  ( -11.70000000000000107, 0.000000000000000000, -20.69999999999999929 ) ) ;
#7001=CARTESIAN_POINT ( 'NONE',  ( -2.981742216678212820, 0.000000000000000000, 0.000000000000000000 ) ) ;
#7075=DIRECTION ( 'NONE',  ( -0.2079116908177431888, 1.197885328332322634E-16, -0.9781476007338091305 ) ) ;
#7086=CARTESIAN_POINT ( 'NONE',  ( -11.99999999999999645, 13.90444123027096879, 0.000000000000000000 ) ) ;
#7095=VECTOR ( 'NONE', #6433, 1000.000000000000114 ) ;
#7096=UNCERTAINTY_MEASURE_WITH_UNIT (LENGTH_MEASURE( 1.000000000000000082E-05 ), #1273, 'distance_accuracy_value', 'NONE');
#7118=EDGE_LOOP ( 'NONE', ( #18750, #14117, #36140, #18395 ) ) ;
#7226=ADVANCED_FACE ( 'NONE', ( #7583, #26183 ), #33514, .T. ) ;
#7269=DIRECTION ( 'NONE',  ( 0.000000000000000000, 0.000000000000000000, -1.000000000000000000 ) ) ;
#7341=CARTESIAN_POINT ( 'NONE',  ( -12.00000000000000000, 2.119128821244579932E-15, 17.30399999999999849 ) ) ;
#7342=AXIS2_PLACEMENT_3D ( 'NONE', #42009, #26826, #41762 ) ;
#7447=CARTESIAN_POINT ( 'NONE',  ( -2.981742216678212820, 0.000000000000000000, 0.000000000000000000 ) ) ;
#7539=CIRCLE ( 'NONE', #46611, 21.00000000000000000 ) ;
#7583=FACE_BOUND ( 'NONE', #23989, .T. ) ;
#7663=CARTESIAN_POINT ( 'NONE',  ( -11.68233973192911535, 0.000000000000000000, 0.000000000000000000 ) ) ;
#7816=ORIENTED_EDGE ( 'NONE', *, *, #12827, .F. ) ;
#7820=CARTESIAN_POINT ( 'NONE',  ( -10.90076147243505211, 0.000000000000000000, 0.000000000000000000 ) ) ;
#7822=EDGE_CURVE ( 'NONE', #1706, #20800, #17474, .T. ) ;
#7830=CIRCLE ( 'NONE', #35195, 15.39727592608509177 ) ;
#7897=EDGE_CURVE ( 'NONE', #14976, #30318, #38220, .T. ) ;
#8011=CIRCLE ( 'NONE', #3293, 13.71319123027096865 ) ;
#8034=CIRCLE ( 'NONE', #11966, 17.30399999999999849 ) ;
#8085=VECTOR ( 'NONE', #15694, 1000.000000000000114 ) ;
#8130=ORIENTED_EDGE ( 'NONE', *, *, #37434, .T. ) ;
#8192=EDGE_CURVE ( 'NONE', #23375, #29705, #27860, .T. ) ;
#8217=DIRECTION ( 'NONE',  ( 0.000000000000000000, 0.000000000000000000, -1.000000000000000000 ) ) ;
#8298=DIRECTION ( 'NONE',  ( 0.9781476007338070211, 0.000000000000000000, -0.2079116908177526257 ) ) ;
#8314=DIRECTION ( 'NONE',  ( 1.000000000000000000, 0.000000000000000000, 0.000000000000000000 ) ) ;
#8354=CIRCLE ( 'NONE', #28691, 0.2999999999999999334 ) ;
#8399=DIRECTION ( 'NONE',  ( 0.000000000000000000, 0.000000000000000000, -1.000000000000000000 ) ) ;
#8453=AXIS2_PLACEMENT_3D ( 'NONE', #7820, #15422, #3910 ) ;
#8472=ORIENTED_EDGE ( 'NONE', *, *, #15593, .T. ) ;
#8529=AXIS2_PLACEMENT_3D ( 'NONE', #44354, #25735, #17911 ) ;
#8540=DIRECTION ( 'NONE',  ( 0.000000000000000000, 0.000000000000000000, -1.000000000000000000 ) ) ;
#8684=EDGE_LOOP ( 'NONE', ( #14838, #17866, #3385, #2259 ) ) ;
#8752=ORIENTED_EDGE ( 'NONE', *, *, #7897, .F. ) ;
#8754=CARTESIAN_POINT ( 'NONE',  ( -42.50000000000000000, 1.702802944658382841E-15, 13.90444123027096879 ) ) ;
#8794=AXIS2_PLACEMENT_3D ( 'NONE', #32156, #43643, #10109 ) ;
#8889=FACE_OUTER_BOUND ( 'NONE', #19207, .T. ) ;
#8908=VERTEX_POINT ( 'NONE', #18678 ) ;
#8938=VERTEX_POINT ( 'NONE', #44875 ) ;
#8981=VERTEX_POINT ( 'NONE', #38989 ) ;
#9035=FACE_BOUND ( 'NONE', #41197, .T. ) ;
#9048=EDGE_CURVE ( 'NONE', #38765, #33441, #3356, .T. ) ;
#9225=ORIENTED_EDGE ( 'NONE', *, *, #29788, .T. ) ;
#9490=ADVANCED_FACE ( 'NONE', ( #13404 ), #47171, .T. ) ;
#9513=EDGE_CURVE ( 'NONE', #48194, #13671, #28579, .T. ) ;
#9587=DIRECTION ( 'NONE',  ( 1.000000000000000000, 0.000000000000000000, 0.000000000000000000 ) ) ;
#9593=EDGE_CURVE ( 'NONE', #8938, #28565, #19773, .T. ) ;
#9599=DIRECTION ( 'NONE',  ( 1.000000000000000000, -0.000000000000000000, -0.000000000000000000 ) ) ;
#9640=CIRCLE ( 'NONE', #37006, 17.30399999999999849 ) ;
#9648=DIRECTION ( 'NONE',  ( -0.2079116908177431888, 0.000000000000000000, 0.9781476007338091305 ) ) ;
#9662=DIRECTION ( 'NONE',  ( 1.000000000000000000, 0.000000000000000000, 0.000000000000000000 ) ) ;
#9686=AXIS2_PLACEMENT_3D ( 'NONE', #11861, #41481, #19424 ) ;
#9689=PRODUCT ( 'taper roller bearing_iso_ISO 355-2 - 2BD25 - 22,SI,NC,22', 'taper roller bearing_iso_ISO 355-2 - 2BD25 - 22,SI,NC,22', '', ( #12537 ) ) ;
#9739=EDGE_CURVE ( 'NONE', #13040, #21273, #16720, .T. ) ;
#9838=AXIS2_PLACEMENT_3D ( 'NONE', #7447, #33616, #3036 ) ;
#9839=EDGE_CURVE ( 'NONE', #8908, #16167, #40166, .T. ) ;
#9848=ORIENTED_EDGE ( 'NONE', *, *, #15593, .F. ) ;
#9886=VERTEX_POINT ( 'NONE', #33916 ) ;
#9888=CIRCLE ( 'NONE', #36439, 13.90444123027096879 ) ;
#9939=CARTESIAN_POINT ( 'NONE',  ( -10.90076147243505211, 0.000000000000000000, 0.000000000000000000 ) ) ;
#9945=EDGE_CURVE ( 'NONE', #28565, #8938, #10462, .T. ) ;
#9987=CARTESIAN_POINT ( 'NONE',  ( -10.94538922500103162, 0.000000000000000000, 0.000000000000000000 ) ) ;
#10004=EDGE_LOOP ( 'NONE', ( #46594, #28977, #24822, #25352 ) ) ;
#10109=DIRECTION ( 'NONE',  ( 0.000000000000000000, 0.000000000000000000, -1.000000000000000000 ) ) ;
#10118=FACE_OUTER_BOUND ( 'NONE', #46979, .T. ) ;
#10127=ORIENTED_EDGE ( 'NONE', *, *, #33805, .F. ) ;
#10242=ORIENTED_EDGE ( 'NONE', *, *, #36889, .F. ) ;
#10340=CIRCLE ( 'NONE', #39269, 13.90444123027096879 ) ;
#10450=CARTESIAN_POINT ( 'NONE',  ( 6.938893903907228378E-15, 0.000000000000000000, 0.000000000000000000 ) ) ;
#10462=CIRCLE ( 'NONE', #1880, 12.50000000000000000 ) ;
#10463=AXIS2_PLACEMENT_3D ( 'NONE', #11462, #26381, #37630 ) ;
#10478=SURFACE_SIDE_STYLE ('',( #10958 ) ) ;
#10515=EDGE_CURVE ( 'NONE', #28565, #30318, #39965, .T. ) ;
#10599=FACE_OUTER_BOUND ( 'NONE', #25779, .T. ) ;
#10685=ORIENTED_EDGE ( 'NONE', *, *, #27036, .F. ) ;
#10723=ADVANCED_FACE ( 'NONE', ( #27, #26717 ), #18639, .T. ) ;
#10851=ORIENTED_EDGE ( 'NONE', *, *, #22397, .T. ) ;
#10856=VECTOR ( 'NONE', #9648, 1000.000000000000114 ) ;
#10958=SURFACE_STYLE_FILL_AREA ( #25633 ) ;
#10971=DIRECTION ( 'NONE',  ( 1.000000000000000000, 0.000000000000000000, 0.000000000000000000 ) ) ;
#11075=CONICAL_SURFACE ( 'NONE', #25139, 20.64000000000000057, 0.7853981633974482790 ) ;
#11098=ORIENTED_EDGE ( 'NONE', *, *, #28327, .T. ) ;
#11103=ORIENTED_EDGE ( 'NONE', *, *, #13668, .F. ) ;
#11268=CONICAL_SURFACE ( 'NONE', #38634, 12.85999999999999943, 0.7853981633974482790 ) ;
#11462=CARTESIAN_POINT ( 'NONE',  ( -3.759344165985237129, 0.000000000000000000, 0.000000000000000000 ) ) ;
#11477=CARTESIAN_POINT ( 'NONE',  ( -11.68233973192911535, 2.127397731264211754E-15, 17.37152077436032371 ) ) ;
#11505=DIRECTION ( 'NONE',  ( -1.000000000000000000, 0.000000000000000000, -0.000000000000000000 ) ) ;
#11581=DIRECTION ( 'NONE',  ( 1.000000000000000000, 0.000000000000000000, 0.000000000000000000 ) ) ;
#11592=DIRECTION ( 'NONE',  ( 0.000000000000000000, 0.000000000000000000, -1.000000000000000000 ) ) ;
#11620=EDGE_CURVE ( 'NONE', #29705, #22027, #23581, .T. ) ;
#11636=AXIS2_PLACEMENT_3D ( 'NONE', #13959, #6619, #3667 ) ;
#11799=CARTESIAN_POINT ( 'NONE',  ( -10.94538922500103162, 1.915100337961297692E-15, -13.90444123027096879 ) ) ;
#11861=CARTESIAN_POINT ( 'NONE',  ( -2.977765906491215642, 0.000000000000000000, 0.000000000000000000 ) ) ;
#11885=VERTEX_POINT ( 'NONE', #23293 ) ;
#11891=AXIS2_PLACEMENT_3D ( 'NONE', #32672, #36351, #13595 ) ;
#11928=EDGE_LOOP ( 'NONE', ( #41881, #8130, #25838, #10242 ) ) ;
#11966=AXIS2_PLACEMENT_3D ( 'NONE', #13465, #5897, #27939 ) ;
#11969=ORIENTED_EDGE ( 'NONE', *, *, #3609, .F. ) ;
#12055=( NAMED_UNIT ( * ) SI_UNIT ( $, .STERADIAN. ) SOLID_ANGLE_UNIT ( ) );
#12071=AXIS2_PLACEMENT_3D ( 'NONE', #31651, #24522, #35544 ) ;
#12075=CARTESIAN_POINT ( 'NONE',  ( 6.938893903907228378E-15, 0.000000000000000000, 0.000000000000000000 ) ) ;
#12078=DIRECTION ( 'NONE',  ( -0.7071067811865474617, 0.000000000000000000, 0.7071067811865474617 ) ) ;
#12108=CARTESIAN_POINT ( 'NONE',  ( -11.99999999999999645, 0.000000000000000000, 0.000000000000000000 ) ) ;
#12128=CARTESIAN_POINT ( 'NONE',  ( -2.981742216678212820, 0.000000000000000000, -15.39727592608509177 ) ) ;
#12192=PRODUCT_DEFINITION ( 'UNKNOWN', '', #20188, #37447 ) ;
#12256=AXIS2_PLACEMENT_3D ( 'NONE', #46153, #633, #8217 ) ;
#12276=EDGE_LOOP ( 'NONE', ( #14116, #1461 ) ) ;
#12337=FACE_OUTER_BOUND ( 'NONE', #20881, .T. ) ;
#12468=TOROIDAL_SURFACE ( 'NONE', #39823, 12.80000000000000071, 0.2999999999999999334 ) ;
#12537=PRODUCT_CONTEXT ( 'NONE', #20072, 'mechanical' ) ;
#12584=CARTESIAN_POINT ( 'NONE',  ( -2.977765906491215642, 1.885622467823562354E-15, 15.39727592589476579 ) ) ;
#12643=EDGE_CURVE ( 'NONE', #30256, #22671, #30809, .T. ) ;
#12658=ORIENTED_EDGE ( 'NONE', *, *, #21216, .F. ) ;
#12675=CARTESIAN_POINT ( 'NONE',  ( -42.50000000000000000, 1.530808498934191521E-15, 12.50000000000000000 ) ) ;
#12697=DIRECTION ( 'NONE',  ( 0.000000000000000000, 0.000000000000000000, -1.000000000000000000 ) ) ;
#12707=CARTESIAN_POINT ( 'NONE',  ( -11.70000000000000107, 0.000000000000000000, 0.000000000000000000 ) ) ;
#12747=EDGE_LOOP ( 'NONE', ( #11969, #31247, #26879, #8752 ) ) ;
#12764=SURFACE_STYLE_FILL_AREA ( #4931 ) ;
#12774=AXIS2_PLACEMENT_3D ( 'NONE', #13164, #20752, #35681 ) ;
#12799=DIRECTION ( 'NONE',  ( 0.000000000000000000, 0.000000000000000000, -1.000000000000000000 ) ) ;
#12827=EDGE_CURVE ( 'NONE', #28374, #29208, #27730, .T. ) ;
#12890=DIRECTION ( 'NONE',  ( 0.000000000000000000, 1.224646799147353207E-16, 1.000000000000000000 ) ) ;
#12894=CARTESIAN_POINT ( 'NONE',  ( -2.977765906491215642, 0.000000000000000000, -15.77977592589476608 ) ) ;
#12984=DIRECTION ( 'NONE',  ( 0.9781476007338070211, 0.000000000000000000, -0.2079116908177527367 ) ) ;
#12995=CIRCLE ( 'NONE', #2026, 17.37152077436032371 ) ;
#13040=VERTEX_POINT ( 'NONE', #34541 ) ;
#13164=CARTESIAN_POINT ( 'NONE',  ( -11.63999999999999702, 0.000000000000000000, 0.000000000000000000 ) ) ;
#13173=EDGE_CURVE ( 'NONE', #34848, #3678, #9640, .T. ) ;
#13192=( LENGTH_UNIT ( ) NAMED_UNIT ( * ) SI_UNIT ( .MILLI., .METRE. ) );
#13251=STYLED_ITEM ( 'NONE', ( #47905 ), #26873 ) ;
#13272=CARTESIAN_POINT ( 'NONE',  ( -3.759344165985237129, 0.000000000000000000, -19.05560546998412974 ) ) ;
#13295=EDGE_CURVE ( 'NONE', #1706, #22671, #22469, .T. ) ;
#13310=CARTESIAN_POINT ( 'NONE',  ( -11.99999999999999645, 0.000000000000000000, 0.000000000000000000 ) ) ;
#13333=EDGE_CURVE ( 'NONE', #33441, #38765, #1052, .T. ) ;
#13334=EDGE_LOOP ( 'NONE', ( #10685, #48073, #31465, #36842 ) ) ;
#13351=CARTESIAN_POINT ( 'NONE',  ( -42.50000000000000000, 0.000000000000000000, -15.77977592589476608 ) ) ;
#13352=FACE_OUTER_BOUND ( 'NONE', #10004, .T. ) ;
#13391=VERTEX_POINT ( 'NONE', #19724 ) ;
#13404=FACE_OUTER_BOUND ( 'NONE', #39279, .T. ) ;
#13465=CARTESIAN_POINT ( 'NONE',  ( -12.00000000000000000, 0.000000000000000000, 0.000000000000000000 ) ) ;
#13552=AXIS2_PLACEMENT_3D ( 'NONE', #6932, #22092, #17932 ) ;
#13595=DIRECTION ( 'NONE',  ( -0.000000000000000000, 0.000000000000000000, 1.000000000000000000 ) ) ;
#13598=CARTESIAN_POINT ( 'NONE',  ( -12.00000000000000000, 2.123263276254396040E-15, 17.30399999999999849 ) ) ;
#13651=CARTESIAN_POINT ( 'NONE',  ( -11.99999999999999645, 2.553388576222231231E-15, 20.69999999999999929 ) ) ;
#13668=EDGE_CURVE ( 'NONE', #9886, #1706, #8011, .T. ) ;
#13671=VERTEX_POINT ( 'NONE', #41013 ) ;
#13816=CARTESIAN_POINT ( 'NONE',  ( -12.00000000000000000, 0.000000000000000000, -17.30399999999999849 ) ) ;
#13922=VERTEX_POINT ( 'NONE', #12128 ) ;
#13959=CARTESIAN_POINT ( 'NONE',  ( 0.000000000000000000, 0.000000000000000000, 0.000000000000000000 ) ) ;
#13985=FACE_OUTER_BOUND ( 'NONE', #13334, .T. ) ;
#14017=DIRECTION ( 'NONE',  ( 1.000000000000000000, 0.000000000000000000, 0.000000000000000000 ) ) ;
#14116=ORIENTED_EDGE ( 'NONE', *, *, #21216, .T. ) ;
#14117=ORIENTED_EDGE ( 'NONE', *, *, #41314, .T. ) ;
#14121=CARTESIAN_POINT ( 'NONE',  ( 5.204170427930421283E-15, 0.000000000000000000, -12.79999999999999893 ) ) ;
#14128=CARTESIAN_POINT ( 'NONE',  ( 5.204170427930421283E-15, 1.567547902908612184E-15, 12.79999999999999893 ) ) ;
#14156=EDGE_CURVE ( 'NONE', #8981, #16167, #1024, .T. ) ;
#14225=DIRECTION ( 'NONE',  ( 0.000000000000000000, 0.000000000000000000, 1.000000000000000000 ) ) ;
#14431=EDGE_LOOP ( 'NONE', ( #2561, #37899, #6640, #24783 ) ) ;
#14457=UNCERTAINTY_MEASURE_WITH_UNIT (LENGTH_MEASURE( 1.000000000000000082E-05 ), #13192, 'distance_accuracy_value', 'NONE');
#14502=DIRECTION ( 'NONE',  ( 0.000000000000000000, 0.000000000000000000, -1.000000000000000000 ) ) ;
#14838=ORIENTED_EDGE ( 'NONE', *, *, #4144, .T. ) ;
#14877=AXIS2_PLACEMENT_3D ( 'NONE', #1860, #42488, #23887 ) ;
#14976=VERTEX_POINT ( 'NONE', #2893 ) ;
#14980=CARTESIAN_POINT ( 'NONE',  ( -12.00000000000000000, 17.30399999999999849, 0.000000000000000000 ) ) ;
#15016=DIRECTION ( 'NONE',  ( -1.000000000000000000, 0.000000000000000000, 0.000000000000000000 ) ) ;
#15136=ORIENTED_EDGE ( 'NONE', *, *, #43617, .F. ) ;
#15174=CARTESIAN_POINT ( 'NONE',  ( -12.00000000000000000, 0.000000000000000000, 0.000000000000000000 ) ) ;
#15204=FACE_OUTER_BOUND ( 'NONE', #31975, .T. ) ;
#15248=CIRCLE ( 'NONE', #372, 0.2999999999999981570 ) ;
#15311=ORIENTED_EDGE ( 'NONE', *, *, #27739, .F. ) ;
#15422=DIRECTION ( 'NONE',  ( -1.000000000000000000, -0.000000000000000000, -0.000000000000000000 ) ) ;
#15424=AXIS2_PLACEMENT_3D ( 'NONE', #25090, #40038, #39570 ) ;
#15553=ORIENTED_EDGE ( 'NONE', *, *, #22397, .F. ) ;
#15593=EDGE_CURVE ( 'NONE', #21273, #13040, #32347, .T. ) ;
#15658=CIRCLE ( 'NONE', #19548, 13.71399988598171049 ) ;
#15694=DIRECTION ( 'NONE',  ( -0.7071067811865474617, 8.659560562354932858E-17, -0.7071067811865474617 ) ) ;
#15754=ORIENTED_EDGE ( 'NONE', *, *, #768, .F. ) ;
#15912=ADVANCED_FACE ( 'NONE', ( #39377 ), #28425, .T. ) ;
#16108=ORIENTED_EDGE ( 'NONE', *, *, #11620, .T. ) ;
#16109=EDGE_LOOP ( 'NONE', ( #36538, #15136 ) ) ;
#16167=VERTEX_POINT ( 'NONE', #38619 ) ;
#16174=ORIENTED_EDGE ( 'NONE', *, *, #31452, .T. ) ;
#16211=ORIENTED_EDGE ( 'NONE', *, *, #13173, .T. ) ;
#16238=DIRECTION ( 'NONE',  ( 1.000000000000000000, 0.000000000000000000, 0.000000000000000000 ) ) ;
#16468=FACE_OUTER_BOUND ( 'NONE', #46938, .T. ) ;
#16606=CARTESIAN_POINT ( 'NONE',  ( -12.00000000000000000, 0.000000000000000000, -17.30399999999999849 ) ) ;
#16668=DIRECTION ( 'NONE',  ( 0.000000000000000000, 0.000000000000000000, -1.000000000000000000 ) ) ;
#16701=CYLINDRICAL_SURFACE ( 'NONE', #12071, 20.99999999999999645 ) ;
#16720=CIRCLE ( 'NONE', #44840, 15.77977592589476608 ) ;
#16877=ORIENTED_EDGE ( 'NONE', *, *, #40347, .F. ) ;
#16977=DIRECTION ( 'NONE',  ( 1.000000000000000000, 0.000000000000000000, 0.000000000000000000 ) ) ;
#17043=DIRECTION ( 'NONE',  ( 0.000000000000000000, 0.000000000000000000, -1.000000000000000000 ) ) ;
#17066=CARTESIAN_POINT ( 'NONE',  ( -42.50000000000000000, 0.000000000000000000, 0.000000000000000000 ) ) ;
#17094=( NAMED_UNIT ( * ) SI_UNIT ( $, .STERADIAN. ) SOLID_ANGLE_UNIT ( ) );
#17123=DIRECTION ( 'NONE',  ( 0.000000000000000000, 0.000000000000000000, -1.000000000000000000 ) ) ;
#17145=CARTESIAN_POINT ( 'NONE',  ( -2.981742216678212820, 0.000000000000000000, 0.000000000000000000 ) ) ;
#17253=DIRECTION ( 'NONE',  ( 0.000000000000000000, 0.000000000000000000, 1.000000000000000000 ) ) ;
#17283=ADVANCED_FACE ( 'NONE', ( #13985 ), #11075, .T. ) ;
#17298=DIRECTION ( 'NONE',  ( 0.000000000000000000, 0.000000000000000000, -1.000000000000000000 ) ) ;
#17395=CIRCLE ( 'NONE', #33054, 12.79999999999999893 ) ;
#17414=DIRECTION ( 'NONE',  ( 1.000000000000000000, 0.000000000000000000, 0.000000000000000000 ) ) ;
#17464=AXIS2_PLACEMENT_3D ( 'NONE', #23828, #19648, #42425 ) ;
#17474=LINE ( 'NONE', #48067, #10856 ) ;
#17533=ORIENTED_EDGE ( 'NONE', *, *, #25012, .F. ) ;
#17568=DIRECTION ( 'NONE',  ( 1.000000000000000000, 0.000000000000000000, 0.000000000000000000 ) ) ;
#17730=DIRECTION ( 'NONE',  ( 1.000000000000000000, 0.000000000000000000, 0.000000000000000000 ) ) ;
#17749=FACE_OUTER_BOUND ( 'NONE', #16109, .T. ) ;
#17757=ORIENTED_EDGE ( 'NONE', *, *, #23951, .T. ) ;
#17866=ORIENTED_EDGE ( 'NONE', *, *, #9513, .T. ) ;
#17896=DIRECTION ( 'NONE',  ( 0.000000000000000000, 0.000000000000000000, -1.000000000000000000 ) ) ;
#17911=DIRECTION ( 'NONE',  ( 0.000000000000000000, 0.000000000000000000, -1.000000000000000000 ) ) ;
#17930=DIRECTION ( 'NONE',  ( 0.000000000000000000, 0.000000000000000000, -1.000000000000000000 ) ) ;
#17932=DIRECTION ( 'NONE',  ( 0.000000000000000000, 0.000000000000000000, -1.000000000000000000 ) ) ;
#18003=ORIENTED_EDGE ( 'NONE', *, *, #41503, .F. ) ;
#18033=EDGE_LOOP ( 'NONE', ( #6606, #10127 ) ) ;
#18234=VECTOR ( 'NONE', #18544, 1000.000000000000000 ) ;
#18283=ADVANCED_FACE ( 'NONE', ( #19882 ), #799, .T. ) ;
#18298=ORIENTED_EDGE ( 'NONE', *, *, #36549, .F. ) ;
#18361=VECTOR ( 'NONE', #7075, 1000.000000000000114 ) ;
#18392=AXIS2_PLACEMENT_3D ( 'NONE', #24782, #17414, #47294 ) ;
#18395=ORIENTED_EDGE ( 'NONE', *, *, #10515, .F. ) ;
#18446=ADVANCED_FACE ( 'NONE', ( #16468 ), #47664, .T. ) ;
#18544=DIRECTION ( 'NONE',  ( 0.9781476007338070211, 2.546183866652750331E-17, 0.2079116908177527367 ) ) ;
#18575=CARTESIAN_POINT ( 'NONE',  ( -11.99999999999999645, 0.000000000000000000, 0.000000000000000000 ) ) ;
#18639=PLANE ( 'NONE',  #21911 ) ;
#18678=CARTESIAN_POINT ( 'NONE',  ( -11.69999999999999929, 2.571758278209441267E-15, 20.99999999999999645 ) ) ;
#18750=ORIENTED_EDGE ( 'NONE', *, *, #9593, .F. ) ;
#18808=CARTESIAN_POINT ( 'NONE',  ( -11.99999999999999645, 0.000000000000000000, 0.000000000000000000 ) ) ;
#18941=DIRECTION ( 'NONE',  ( 0.000000000000000000, 0.000000000000000000, -1.000000000000000000 ) ) ;
#19000=EDGE_CURVE ( 'NONE', #29208, #28374, #38359, .T. ) ;
#19094=CARTESIAN_POINT ( 'NONE',  ( -11.99999999999999645, 0.000000000000000000, 0.000000000000000000 ) ) ;
#19171=AXIS2_PLACEMENT_3D ( 'NONE', #36759, #14017, #28934 ) ;
#19207=EDGE_LOOP ( 'NONE', ( #21794, #42265, #3209, #33487 ) ) ;
#19315=ORIENTED_EDGE ( 'NONE', *, *, #14156, .T. ) ;
#19346=VERTEX_POINT ( 'NONE', #14128 ) ;
#19423=FACE_OUTER_BOUND ( 'NONE', #8684, .T. ) ;
#19424=DIRECTION ( 'NONE',  ( 0.000000000000000000, 0.000000000000000000, -1.000000000000000000 ) ) ;
#19521=AXIS2_PLACEMENT_3D ( 'NONE', #1467, #35946, #31831 ) ;
#19548=AXIS2_PLACEMENT_3D ( 'NONE', #1099, #41502, #27301 ) ;
#19578=CARTESIAN_POINT ( 'NONE',  ( -2.981742216678212820, 1.885622467846870828E-15, -15.39727592608509177 ) ) ;
#19600=ADVANCED_FACE ( 'NONE', ( #13352 ), #20438, .T. ) ;
#19648=DIRECTION ( 'NONE',  ( -1.000000000000000000, 0.000000000000000000, 0.000000000000000000 ) ) ;
#19724=CARTESIAN_POINT ( 'NONE',  ( -3.360000000000002096, 0.000000000000000000, -21.00000000000000000 ) ) ;
#19773=CIRCLE ( 'NONE', #12774, 12.50000000000000000 ) ;
#19807=AXIS2_PLACEMENT_3D ( 'NONE', #1941, #17568, #20518 ) ;
#19848=DIRECTION ( 'NONE',  ( -0.2079116908177587875, 0.000000000000000000, 0.9781476007338056888 ) ) ;
#19849=SURFACE_SIDE_STYLE ('',( #12764 ) ) ;
#19854=CARTESIAN_POINT ( 'NONE',  ( -12.00000000000000000, 0.000000000000000000, 0.000000000000000000 ) ) ;
#19882=FACE_OUTER_BOUND ( 'NONE', #11928, .T. ) ;
#19895=LINE ( 'NONE', #41698, #24643 ) ;
#19967=CIRCLE ( 'NONE', #18392, 13.71399988598171049 ) ;
#20072=APPLICATION_CONTEXT ( 'automotive_design' ) ;
#20145=( GEOMETRIC_REPRESENTATION_CONTEXT ( 3 ) GLOBAL_UNCERTAINTY_ASSIGNED_CONTEXT ( ( #7096 ) ) GLOBAL_UNIT_ASSIGNED_CONTEXT ( ( #1273, #24029, #12055 ) ) REPRESENTATION_CONTEXT ( 'NONE', 'WORKASPACE' ) );
#20188=PRODUCT_DEFINITION_FORMATION_WITH_SPECIFIED_SOURCE ( 'ANY', '', #9689, .NOT_KNOWN. ) ;
#20272=LINE ( 'NONE', #1685, #40102 ) ;
#20438=CYLINDRICAL_SURFACE ( 'NONE', #14877, 13.90444123027096879 ) ;
#20486=CARTESIAN_POINT ( 'NONE',  ( -3.360000000000002096, 0.000000000000000000, 0.000000000000000000 ) ) ;
#20518=DIRECTION ( 'NONE',  ( 0.000000000000000000, 0.000000000000000000, -1.000000000000000000 ) ) ;
#20558=CARTESIAN_POINT ( 'NONE',  ( -10.90076147243505211, 0.000000000000000000, 13.71319123027096865 ) ) ;
#20650=VERTEX_POINT ( 'NONE', #13651 ) ;
#20725=DIRECTION ( 'NONE',  ( 1.000000000000000000, 0.000000000000000000, 0.000000000000000000 ) ) ;
#20752=DIRECTION ( 'NONE',  ( 1.000000000000000000, 0.000000000000000000, 0.000000000000000000 ) ) ;
#20800=VERTEX_POINT ( 'NONE', #25852 ) ;
#20836=ORIENTED_EDGE ( 'NONE', *, *, #45048, .F. ) ;
#20867=DIRECTION ( 'NONE',  ( 1.000000000000000000, 0.000000000000000000, 0.000000000000000000 ) ) ;
#20881=EDGE_LOOP ( 'NONE', ( #41516, #3143, #36730, #1280 ) ) ;
#20892=CARTESIAN_POINT ( 'NONE',  ( -11.70000000000000107, 2.137572712735109784E-15, -17.45460580326810174 ) ) ;
#20937=DIRECTION ( 'NONE',  ( 1.000000000000000000, 0.000000000000000000, 0.000000000000000000 ) ) ;
#20941=CARTESIAN_POINT ( 'NONE',  ( -11.70000000000000107, 0.000000000000000000, 17.45460580326810174 ) ) ;
#21039=VECTOR ( 'NONE', #10971, 1000.000000000000000 ) ;
#21045=CARTESIAN_POINT ( 'NONE',  ( -11.99999999999999645, 1.574895783703496238E-15, -12.85999999999999943 ) ) ;
#21132=DIRECTION ( 'NONE',  ( 0.000000000000000000, 0.000000000000000000, -1.000000000000000000 ) ) ;
#21139=EDGE_CURVE ( 'NONE', #13671, #38915, #6023, .T. ) ;
#21154=ORIENTED_EDGE ( 'NONE', *, *, #33210, .T. ) ;
#21202=DIRECTION ( 'NONE',  ( 0.9781476007338069101, 2.546183866652752180E-17, 0.2079116908177528755 ) ) ;
#21206=DIRECTION ( 'NONE',  ( 0.000000000000000000, 0.000000000000000000, -1.000000000000000000 ) ) ;
#21216=EDGE_CURVE ( 'NONE', #44810, #44505, #47084, .T. ) ;
#21247=VECTOR ( 'NONE', #26299, 1000.000000000000000 ) ;
#21273=VERTEX_POINT ( 'NONE', #26047 ) ;
#21352=PLANE ( 'NONE',  #19171 ) ;
#21742=EDGE_CURVE ( 'NONE', #37732, #13922, #20272, .T. ) ;
#21794=ORIENTED_EDGE ( 'NONE', *, *, #11620, .F. ) ;
#21901=DIRECTION ( 'NONE',  ( 0.000000000000000000, 0.000000000000000000, -1.000000000000000000 ) ) ;
#21911=AXIS2_PLACEMENT_3D ( 'NONE', #14980, #4206, #30397 ) ;
#21949=AXIS2_PLACEMENT_3D ( 'NONE', #43153, #9599, #38269 ) ;
#22027=VERTEX_POINT ( 'NONE', #37617 ) ;
#22063=LINE ( 'NONE', #26239, #8085 ) ;
#22081=CIRCLE ( 'NONE', #36191, 19.21700905503013601 ) ;
#22092=DIRECTION ( 'NONE',  ( 0.000000000000000000, -1.000000000000000000, 0.000000000000000000 ) ) ;
#22141=AXIS2_PLACEMENT_3D ( 'NONE', #36319, #36553, #21132 ) ;
#22167=CIRCLE ( 'NONE', #44853, 20.69999999999999929 ) ;
#22185=DIRECTION ( 'NONE',  ( 0.000000000000000000, 1.224646799147347784E-16, 1.000000000000000000 ) ) ;
#22216=CIRCLE ( 'NONE', #32393, 12.50000000000000000 ) ;
#22219=CARTESIAN_POINT ( 'NONE',  ( -2.977765906491215642, 1.885622467823562354E-15, 15.39727592589476579 ) ) ;
#22392=FACE_OUTER_BOUND ( 'NONE', #40388, .T. ) ;
#22397=EDGE_CURVE ( 'NONE', #27937, #13040, #2109, .T. ) ;
#22431=ORIENTED_EDGE ( 'NONE', *, *, #9593, .T. ) ;
#22469=LINE ( 'NONE', #22219, #18234 ) ;
#22671=VERTEX_POINT ( 'NONE', #12584 ) ;
#22705=VERTEX_POINT ( 'NONE', #28722 ) ;
#22751=AXIS2_PLACEMENT_3D ( 'NONE', #6121, #35966, #17123 ) ;
#22809=SHAPE_REPRESENTATION ( 'taper roller bearing_iso_ISO 355-2 - 2BD25 - 22,SI,NC,22', ( #11636 ), #2952 ) ;
#22894=ORIENTED_EDGE ( 'NONE', *, *, #5152, .F. ) ;
#22921=VECTOR ( 'NONE', #47970, 1000.000000000000114 ) ;
#22959=ORIENTED_EDGE ( 'NONE', *, *, #42830, .F. ) ;
#22986=CIRCLE ( 'NONE', #23744, 17.37152077436032371 ) ;
#22991=DIRECTION ( 'NONE',  ( 1.000000000000000000, 0.000000000000000000, 0.000000000000000000 ) ) ;
#23002=AXIS2_PLACEMENT_3D ( 'NONE', #46089, #4961, #31415 ) ;
#23091=ORIENTED_EDGE ( 'NONE', *, *, #19000, .T. ) ;
#23097=EDGE_CURVE ( 'NONE', #22705, #33441, #26984, .T. ) ;
#23169=ADVANCED_FACE ( 'NONE', ( #5661 ), #34737, .T. ) ;
#23223=CARTESIAN_POINT ( 'NONE',  ( -2.977765906491215642, 0.000000000000000000, 0.000000000000000000 ) ) ;
#23293=CARTESIAN_POINT ( 'NONE',  ( -3.360000000000002096, 2.571758278209441661E-15, 21.00000000000000000 ) ) ;
#23308=CONICAL_SURFACE ( 'NONE', #8453, 13.71319123027096865, 1.361356816555593596 ) ;
#23363=ORIENTED_EDGE ( 'NONE', *, *, #9839, .T. ) ;
#23375=VERTEX_POINT ( 'NONE', #43813 ) ;
#23449=ORIENTED_EDGE ( 'NONE', *, *, #40256, .F. ) ;
#23581=LINE ( 'NONE', #20892, #557 ) ;
#23744=AXIS2_PLACEMENT_3D ( 'NONE', #7663, #15016, #26512 ) ;
#23777=CARTESIAN_POINT ( 'NONE',  ( -11.99999999999999645, 1.702802944658382841E-15, 13.90444123027096879 ) ) ;
#23815=AXIS2_PLACEMENT_3D ( 'NONE', #17145, #24745, #35755 ) ;
#23828=CARTESIAN_POINT ( 'NONE',  ( -11.70000000000000107, 0.000000000000000000, 0.000000000000000000 ) ) ;
#23887=DIRECTION ( 'NONE',  ( 0.000000000000000000, 0.000000000000000000, -1.000000000000000000 ) ) ;
#23909=ORIENTED_EDGE ( 'NONE', *, *, #41476, .F. ) ;
#23914=CONICAL_SURFACE ( 'NONE', #27845, 13.71319123027096865, 1.361356816555593596 ) ;
#23933=LINE ( 'NONE', #12675, #42326 ) ;
#23951=EDGE_CURVE ( 'NONE', #20800, #37732, #19967, .T. ) ;
#23961=DIRECTION ( 'NONE',  ( 1.000000000000000000, 0.000000000000000000, 0.000000000000000000 ) ) ;
#23989=EDGE_LOOP ( 'NONE', ( #23091, #44540 ) ) ;
#24026=ORIENTED_EDGE ( 'NONE', *, *, #7822, .T. ) ;
#24029=( NAMED_UNIT ( * ) PLANE_ANGLE_UNIT ( ) SI_UNIT ( $, .RADIAN. ) );
#24203=EDGE_CURVE ( 'NONE', #9886, #30256, #35235, .T. ) ;
#24235=ORIENTED_EDGE ( 'NONE', *, *, #6163, .F. ) ;
#24299=CARTESIAN_POINT ( 'NONE',  ( -3.000000000000002665, 2.549714635824789697E-15, -20.64000000000000057 ) ) ;
#24309=EDGE_CURVE ( 'NONE', #38915, #22027, #12995, .T. ) ;
#24400=DIRECTION ( 'NONE',  ( 1.000000000000000000, 0.000000000000000000, 0.000000000000000000 ) ) ;
#24483=ORIENTED_EDGE ( 'NONE', *, *, #43617, .T. ) ;
#24500=EDGE_LOOP ( 'NONE', ( #25946, #12658, #28852, #1440 ) ) ;
#24501=AXIS2_PLACEMENT_3D ( 'NONE', #12707, #22991, #27639 ) ;
#24522=DIRECTION ( 'NONE',  ( 1.000000000000000000, 0.000000000000000000, 0.000000000000000000 ) ) ;
#24589=CARTESIAN_POINT ( 'NONE',  ( -10.90076147243505211, 0.000000000000000000, 0.000000000000000000 ) ) ;
#24643=VECTOR ( 'NONE', #30443, 1000.000000000000114 ) ;
#24666=DIRECTION ( 'NONE',  ( 1.000000000000000000, 0.000000000000000000, 0.000000000000000000 ) ) ;
#24709=EDGE_CURVE ( 'NONE', #11885, #13391, #7539, .T. ) ;
#24745=DIRECTION ( 'NONE',  ( -1.000000000000000000, 0.000000000000000000, 0.000000000000000000 ) ) ;
#24782=CARTESIAN_POINT ( 'NONE',  ( -10.90093335751250692, 0.000000000000000000, 0.000000000000000000 ) ) ;
#24783=ORIENTED_EDGE ( 'NONE', *, *, #13333, .T. ) ;
#24822=ORIENTED_EDGE ( 'NONE', *, *, #8192, .T. ) ;
#24838=CARTESIAN_POINT ( 'NONE',  ( -11.70000000000000107, 0.000000000000000000, 0.000000000000000000 ) ) ;
#24855=FACE_OUTER_BOUND ( 'NONE', #24500, .T. ) ;
#24864=DIRECTION ( 'NONE',  ( 1.000000000000000000, 0.000000000000000000, 0.000000000000000000 ) ) ;
#24922=SHAPE_REPRESENTATION_RELATIONSHIP ( 'NONE' , 'NONE' ,  #22809, #26873 ) ;
#25012=EDGE_CURVE ( 'NONE', #16167, #8908, #548, .T. ) ;
#25047=FACE_OUTER_BOUND ( 'NONE', #44557, .T. ) ;
#25090=CARTESIAN_POINT ( 'NONE',  ( -3.000000000000002665, 0.000000000000000000, 0.000000000000000000 ) ) ;
#25105=DIRECTION ( 'NONE',  ( 0.9781476007338070211, 2.546183866652749098E-17, 0.2079116908177526257 ) ) ;
#25123=AXIS2_PLACEMENT_3D ( 'NONE', #39830, #24400, #28318 ) ;
#25139=AXIS2_PLACEMENT_3D ( 'NONE', #44085, #29407, #14225 ) ;
#25151=DIRECTION ( 'NONE',  ( -1.000000000000000000, 0.000000000000000000, 0.000000000000000000 ) ) ;
#25176=DIRECTION ( 'NONE',  ( 1.000000000000000000, 0.000000000000000000, 0.000000000000000000 ) ) ;
#25233=ORIENTED_EDGE ( 'NONE', *, *, #45048, .T. ) ;
#25352=ORIENTED_EDGE ( 'NONE', *, *, #30386, .T. ) ;
#25633=FILL_AREA_STYLE ('',( #33234 ) ) ;
#25646=EDGE_LOOP ( 'NONE', ( #15754, #26233 ) ) ;
#25735=DIRECTION ( 'NONE',  ( 1.000000000000000000, 0.000000000000000000, 0.000000000000000000 ) ) ;
#25738=MECHANICAL_DESIGN_GEOMETRIC_PRESENTATION_REPRESENTATION('',(#13251),#42946);
#25779=EDGE_LOOP ( 'NONE', ( #8472, #26507 ) ) ;
#25838=ORIENTED_EDGE ( 'NONE', *, *, #45162, .F. ) ;
#25852=CARTESIAN_POINT ( 'NONE',  ( -10.90093335751250692, 1.782551537117168429E-15, 13.71399988598171049 ) ) ;
#25868=CYLINDRICAL_SURFACE ( 'NONE', #45947, 12.50000000000000000 ) ;
#25875=SURFACE_STYLE_USAGE ( .BOTH. , #10478 ) ;
#25906=ORIENTED_EDGE ( 'NONE', *, *, #13333, .F. ) ;
#25946=ORIENTED_EDGE ( 'NONE', *, *, #5597, .F. ) ;
#26047=CARTESIAN_POINT ( 'NONE',  ( 6.938893903907228378E-15, 0.000000000000000000, -15.77977592589476608 ) ) ;
#26183=FACE_OUTER_BOUND ( 'NONE', #18033, .T. ) ;
#26233=ORIENTED_EDGE ( 'NONE', *, *, #37250, .F. ) ;
#26239=CARTESIAN_POINT ( 'NONE',  ( -3.000000000000002665, 2.527670993440137339E-15, -20.64000000000000057 ) ) ;
#26299=DIRECTION ( 'NONE',  ( -0.2079116908177527367, 0.000000000000000000, 0.9781476007338070211 ) ) ;
#26381=DIRECTION ( 'NONE',  ( 1.000000000000000000, -0.000000000000000000, -0.000000000000000000 ) ) ;
#26431=DIRECTION ( 'NONE',  ( -0.000000000000000000, 0.000000000000000000, 1.000000000000000000 ) ) ;
#26449=ORIENTED_EDGE ( 'NONE', *, *, #38304, .T. ) ;
#26450=EDGE_LOOP ( 'NONE', ( #3670, #39668, #19315, #37696 ) ) ;
#26489=EDGE_CURVE ( 'NONE', #46875, #21273, #46651, .T. ) ;
#26507=ORIENTED_EDGE ( 'NONE', *, *, #9739, .T. ) ;
#26512=DIRECTION ( 'NONE',  ( 0.000000000000000000, 0.000000000000000000, 1.000000000000000000 ) ) ;
#26531=CARTESIAN_POINT ( 'NONE',  ( -2.981742216678212820, 0.000000000000000000, 0.000000000000000000 ) ) ;
#26581=AXIS2_PLACEMENT_3D ( 'NONE', #38992, #9587, #46328 ) ;
#26617=VECTOR ( 'NONE', #2744, 1000.000000000000000 ) ;
#26641=CIRCLE ( 'NONE', #32877, 19.21700905503013601 ) ;
#26643=CARTESIAN_POINT ( 'NONE',  ( 6.938893903907228378E-15, 0.000000000000000000, 0.000000000000000000 ) ) ;
#26670=DIRECTION ( 'NONE',  ( 1.000000000000000000, 0.000000000000000000, 0.000000000000000000 ) ) ;
#26672=FACE_OUTER_BOUND ( 'NONE', #28844, .T. ) ;
#26677=UNCERTAINTY_MEASURE_WITH_UNIT (LENGTH_MEASURE( 1.000000000000000082E-05 ), #2630, 'distance_accuracy_value', 'NONE');
#26702=ORIENTED_EDGE ( 'NONE', *, *, #33033, .T. ) ;
#26717=FACE_OUTER_BOUND ( 'NONE', #43710, .T. ) ;
#26759=CARTESIAN_POINT ( 'NONE',  ( -42.50000000000000000, 0.000000000000000000, 0.000000000000000000 ) ) ;
#26767=DIRECTION ( 'NONE',  ( 1.000000000000000000, -0.000000000000000000, -0.000000000000000000 ) ) ;
#26826=DIRECTION ( 'NONE',  ( 1.000000000000000000, 0.000000000000000000, 0.000000000000000000 ) ) ;
#26873=ADVANCED_BREP_SHAPE_REPRESENTATION ( '', ( #35540, #11636 ), #2952 ) ;
#26879=ORIENTED_EDGE ( 'NONE', *, *, #42830, .T. ) ;
#26923=CARTESIAN_POINT ( 'NONE',  ( -11.99999999999999645, 0.000000000000000000, 0.000000000000000000 ) ) ;
#26964=LINE ( 'NONE', #19578, #42593 ) ;
#26984=LINE ( 'NONE', #1272, #28500 ) ;
#27036=EDGE_CURVE ( 'NONE', #44505, #44810, #33542, .T. ) ;
#27124=AXIS2_PLACEMENT_3D ( 'NONE', #31983, #5059, #17253 ) ;
#27165=CONICAL_SURFACE ( 'NONE', #15424, 20.64000000000000057, 0.7853981633974482790 ) ;
#27178=ORIENTED_EDGE ( 'NONE', *, *, #44319, .T. ) ;
#27206=DIRECTION ( 'NONE',  ( 0.000000000000000000, 0.000000000000000000, -1.000000000000000000 ) ) ;
#27218=MECHANICAL_DESIGN_GEOMETRIC_PRESENTATION_REPRESENTATION('',(#34989),#20145);
#27301=DIRECTION ( 'NONE',  ( 0.000000000000000000, 0.000000000000000000, 1.000000000000000000 ) ) ;
#27452=DIRECTION ( 'NONE',  ( 1.000000000000000000, 0.000000000000000000, 0.000000000000000000 ) ) ;
#27495=FACE_OUTER_BOUND ( 'NONE', #45553, .T. ) ;
#27639=DIRECTION ( 'NONE',  ( 0.000000000000000000, 0.000000000000000000, -1.000000000000000000 ) ) ;
#27652=CONICAL_SURFACE ( 'NONE', #17464, 17.45460580326810174, 1.361356816555583826 ) ;
#27655=ORIENTED_EDGE ( 'NONE', *, *, #21742, .T. ) ;
#27730=CIRCLE ( 'NONE', #30062, 12.85999999999999943 ) ;
#27737=CARTESIAN_POINT ( 'NONE',  ( -12.00000000000000000, 0.000000000000000000, 0.000000000000000000 ) ) ;
#27739=EDGE_CURVE ( 'NONE', #37732, #20800, #15658, .T. ) ;
#27769=ORIENTED_EDGE ( 'NONE', *, *, #29788, .F. ) ;
#27810=CARTESIAN_POINT ( 'NONE',  ( -11.63999999999999702, 0.000000000000000000, 0.000000000000000000 ) ) ;
#27845=AXIS2_PLACEMENT_3D ( 'NONE', #38461, #1002, #4924 ) ;
#27860=LINE ( 'NONE', #5087, #32683 ) ;
#27874=DIRECTION ( 'NONE',  ( 1.000000000000000000, 0.000000000000000000, 0.000000000000000000 ) ) ;
#27878=ORIENTED_EDGE ( 'NONE', *, *, #24309, .F. ) ;
#27926=CONICAL_SURFACE ( 'NONE', #39663, 17.30399999999999849, 0.2094395102393129815 ) ;
#27937=VERTEX_POINT ( 'NONE', #31951 ) ;
#27939=DIRECTION ( 'NONE',  ( 0.000000000000000000, 0.000000000000000000, -1.000000000000000000 ) ) ;
#28117=( NAMED_UNIT ( * ) PLANE_ANGLE_UNIT ( ) SI_UNIT ( $, .RADIAN. ) );
#28136=AXIS2_PLACEMENT_3D ( 'NONE', #24589, #2781, #43668 ) ;
#28191=FACE_OUTER_BOUND ( 'NONE', #43016, .T. ) ;
#28233=DIRECTION ( 'NONE',  ( 0.000000000000000000, 0.000000000000000000, -1.000000000000000000 ) ) ;
#28244=VECTOR ( 'NONE', #21202, 1000.000000000000114 ) ;
#28281=FACE_BOUND ( 'NONE', #38155, .T. ) ;
#28285=DIRECTION ( 'NONE',  ( 0.000000000000000000, 1.000000000000000000, -1.224646799147353207E-16 ) ) ;
#28318=DIRECTION ( 'NONE',  ( 0.000000000000000000, 0.000000000000000000, -1.000000000000000000 ) ) ;
#28327=EDGE_CURVE ( 'NONE', #34848, #22027, #2052, .T. ) ;
#28374=VERTEX_POINT ( 'NONE', #28929 ) ;
#28376=AXIS2_PLACEMENT_3D ( 'NONE', #41053, #37845, #29537 ) ;
#28382=FACE_OUTER_BOUND ( 'NONE', #37343, .T. ) ;
#28425=TOROIDAL_SURFACE ( 'NONE', #19807, 12.80000000000000071, 0.2999999999999999334 ) ;
#28438=ORIENTED_EDGE ( 'NONE', *, *, #5528, .F. ) ;
#28457=CARTESIAN_POINT ( 'NONE',  ( -42.50000000000000000, 0.000000000000000000, -12.50000000000000000 ) ) ;
#28500=VECTOR ( 'NONE', #19848, 1000.000000000000114 ) ;
#28537=DIRECTION ( 'NONE',  ( 1.000000000000000000, 0.000000000000000000, 0.000000000000000000 ) ) ;
#28565=VERTEX_POINT ( 'NONE', #44590 ) ;
#28579=LINE ( 'NONE', #8754, #43274 ) ;
#28691=AXIS2_PLACEMENT_3D ( 'NONE', #1870, #28285, #12890 ) ;
#28722=CARTESIAN_POINT ( 'NONE',  ( -2.981742216678212820, 1.885622467846870828E-15, 15.39727592608509177 ) ) ;
#28832=ORIENTED_EDGE ( 'NONE', *, *, #5528, .T. ) ;
#28844=EDGE_LOOP ( 'NONE', ( #11103, #21154, #44471, #46943 ) ) ;
#28852=ORIENTED_EDGE ( 'NONE', *, *, #40404, .T. ) ;
#28929=CARTESIAN_POINT ( 'NONE',  ( -11.99999999999999645, 1.574895783703496238E-15, -12.85999999999999943 ) ) ;
#28934=DIRECTION ( 'NONE',  ( 0.000000000000000000, 0.000000000000000000, -1.000000000000000000 ) ) ;
#28977=ORIENTED_EDGE ( 'NONE', *, *, #33805, .T. ) ;
#28991=DIRECTION ( 'NONE',  ( 0.000000000000000000, 0.000000000000000000, -1.000000000000000000 ) ) ;
#29116=ADVANCED_FACE ( 'NONE', ( #28281, #17749 ), #32210, .T. ) ;
#29133=APPLICATION_CONTEXT ( 'automotive_design' ) ;
#29208=VERTEX_POINT ( 'NONE', #39797 ) ;
#29318=FACE_OUTER_BOUND ( 'NONE', #43930, .T. ) ;
#29407=DIRECTION ( 'NONE',  ( -1.000000000000000000, -0.000000000000000000, -0.000000000000000000 ) ) ;
#29458=LINE ( 'NONE', #13816, #32355 ) ;
#29537=DIRECTION ( 'NONE',  ( 0.000000000000000000, 0.000000000000000000, -1.000000000000000000 ) ) ;
#29644=ADVANCED_FACE ( 'NONE', ( #6920 ), #35579, .F. ) ;
#29668=DIRECTION ( 'NONE',  ( 1.000000000000000000, 0.000000000000000000, 0.000000000000000000 ) ) ;
#29705=VERTEX_POINT ( 'NONE', #11799 ) ;
#29744=CONICAL_SURFACE ( 'NONE', #33649, 12.85999999999999943, 0.7853981633974482790 ) ;
#29769=CYLINDRICAL_SURFACE ( 'NONE', #22751, 15.77977592589476608 ) ;
#29788=EDGE_CURVE ( 'NONE', #37954, #6365, #22081, .T. ) ;
#29802=ORIENTED_EDGE ( 'NONE', *, *, #12643, .F. ) ;
#29806=AXIS2_PLACEMENT_3D ( 'NONE', #39667, #25176, #39889 ) ;
#29833=ORIENTED_EDGE ( 'NONE', *, *, #41314, .F. ) ;
#30032=CIRCLE ( 'NONE', #2646, 15.77977592589476608 ) ;
#30062=AXIS2_PLACEMENT_3D ( 'NONE', #13310, #16977, #28233 ) ;
#30094=CARTESIAN_POINT ( 'NONE',  ( -3.360000000000002096, 0.000000000000000000, 0.000000000000000000 ) ) ;
#30099=DIRECTION ( 'NONE',  ( 1.000000000000000000, 0.000000000000000000, 0.000000000000000000 ) ) ;
#30158=AXIS2_PLACEMENT_3D ( 'NONE', #12108, #1062, #818 ) ;
#30225=DIRECTION ( 'NONE',  ( 1.000000000000000000, 0.000000000000000000, 0.000000000000000000 ) ) ;
#30256=VERTEX_POINT ( 'NONE', #46235 ) ;
#30280=ADVANCED_FACE ( 'NONE', ( #35212, #9035 ), #5129, .T. ) ;
#30318=VERTEX_POINT ( 'NONE', #34723 ) ;
#30348=ADVANCED_FACE ( 'NONE', ( #4876 ), #45592, .T. ) ;
#30386=EDGE_CURVE ( 'NONE', #29705, #13671, #278, .T. ) ;
#30397=DIRECTION ( 'NONE',  ( -0.000000000000000000, 0.000000000000000000, 1.000000000000000000 ) ) ;
#30443=DIRECTION ( 'NONE',  ( -0.7071067811865474617, 0.000000000000000000, 0.7071067811865474617 ) ) ;
#30566=DIRECTION ( 'NONE',  ( 1.000000000000000000, 0.000000000000000000, 0.000000000000000000 ) ) ;
#30645=ORIENTED_EDGE ( 'NONE', *, *, #13295, .F. ) ;
#30678=ORIENTED_EDGE ( 'NONE', *, *, #31510, .T. ) ;
#30775=ORIENTED_EDGE ( 'NONE', *, *, #9739, .F. ) ;
#30809=CIRCLE ( 'NONE', #9686, 15.39727592589476579 ) ;
#30857=ADVANCED_FACE ( 'NONE', ( #10118 ), #45557, .F. ) ;
#31212=ORIENTED_EDGE ( 'NONE', *, *, #1704, .F. ) ;
#31227=ORIENTED_EDGE ( 'NONE', *, *, #3609, .T. ) ;
#31247=ORIENTED_EDGE ( 'NONE', *, *, #37250, .T. ) ;
#31285=DIRECTION ( 'NONE',  ( 1.000000000000000000, 0.000000000000000000, 0.000000000000000000 ) ) ;
#31308=CIRCLE ( 'NONE', #19521, 12.79999999999999893 ) ;
#31319=AXIS2_PLACEMENT_3D ( 'NONE', #18575, #2917, #36451 ) ;
#31415=DIRECTION ( 'NONE',  ( 0.000000000000000000, 0.000000000000000000, 1.000000000000000000 ) ) ;
#31452=EDGE_CURVE ( 'NONE', #33441, #6365, #37686, .T. ) ;
#31465=ORIENTED_EDGE ( 'NONE', *, *, #45162, .T. ) ;
#31471=ORIENTED_EDGE ( 'NONE', *, *, #9048, .F. ) ;
#31479=DIRECTION ( 'NONE',  ( 0.000000000000000000, 0.000000000000000000, -1.000000000000000000 ) ) ;
#31510=EDGE_CURVE ( 'NONE', #8981, #20650, #37875, .T. ) ;
#31599=ORIENTED_EDGE ( 'NONE', *, *, #31510, .F. ) ;
#31606=ORIENTED_EDGE ( 'NONE', *, *, #5152, .T. ) ;
#31639=AXIS2_PLACEMENT_3D ( 'NONE', #26923, #8314, #8540 ) ;
#31644=DIRECTION ( 'NONE',  ( 1.000000000000000000, 0.000000000000000000, 0.000000000000000000 ) ) ;
#31651=CARTESIAN_POINT ( 'NONE',  ( -42.50000000000000000, 0.000000000000000000, 0.000000000000000000 ) ) ;
#31831=DIRECTION ( 'NONE',  ( 0.000000000000000000, 0.000000000000000000, -1.000000000000000000 ) ) ;
#31928=DIRECTION ( 'NONE',  ( -0.2079116908177527367, 1.197885328332319922E-16, -0.9781476007338070211 ) ) ;
#31951=CARTESIAN_POINT ( 'NONE',  ( -2.977765906491215642, 1.932465207890948911E-15, 15.77977592589476608 ) ) ;
#31975=EDGE_LOOP ( 'NONE', ( #20836, #43782, #27178, #7816 ) ) ;
#31983=CARTESIAN_POINT ( 'NONE',  ( -11.70000000000000107, 0.000000000000000000, 0.000000000000000000 ) ) ;
#32011=ORIENTED_EDGE ( 'NONE', *, *, #26489, .T. ) ;
#32114=CARTESIAN_POINT ( 'NONE',  ( -42.50000000000000000, 0.000000000000000000, -20.99999999999999645 ) ) ;
#32119=EDGE_CURVE ( 'NONE', #20650, #8908, #15248, .T. ) ;
#32147=CARTESIAN_POINT ( 'NONE',  ( -12.00000000000000000, 0.000000000000000000, -17.30399999999999849 ) ) ;
#32156=CARTESIAN_POINT ( 'NONE',  ( -42.50000000000000000, 0.000000000000000000, 0.000000000000000000 ) ) ;
#32165=CIRCLE ( 'NONE', #29806, 15.77977592589476608 ) ;
#32206=CONICAL_SURFACE ( 'NONE', #47792, 17.30399999999999849, 0.2094395102393129815 ) ;
#32210=PLANE ( 'NONE',  #11891 ) ;
#32334=AXIS2_PLACEMENT_3D ( 'NONE', #34972, #26670, #41598 ) ;
#32338=ADVANCED_FACE ( 'NONE', ( #43917 ), #38730, .T. ) ;
#32347=CIRCLE ( 'NONE', #46429, 15.77977592589476608 ) ;
#32355=VECTOR ( 'NONE', #36784, 1000.000000000000114 ) ;
#32393=AXIS2_PLACEMENT_3D ( 'NONE', #34464, #23961, #12697 ) ;
#32466=EDGE_CURVE ( 'NONE', #22705, #13922, #44191, .T. ) ;
#32519=EDGE_LOOP ( 'NONE', ( #34925, #31227, #24235, #22959 ) ) ;
#32672=CARTESIAN_POINT ( 'NONE',  ( -2.977765906491215642, 15.77977592589476608, 0.000000000000000000 ) ) ;
#32683=VECTOR ( 'NONE', #5816, 1000.000000000000000 ) ;
#32877=AXIS2_PLACEMENT_3D ( 'NONE', #48011, #36517, #14502 ) ;
#32942=DIRECTION ( 'NONE',  ( 0.000000000000000000, 0.000000000000000000, 1.000000000000000000 ) ) ;
#33026=VECTOR ( 'NONE', #20937, 1000.000000000000000 ) ;
#33033=EDGE_CURVE ( 'NONE', #13922, #38765, #26964, .T. ) ;
#33054=AXIS2_PLACEMENT_3D ( 'NONE', #26643, #38146, #37655 ) ;
#33117=ORIENTED_EDGE ( 'NONE', *, *, #24203, .F. ) ;
#33196=FACE_OUTER_BOUND ( 'NONE', #36053, .T. ) ;
#33197=CIRCLE ( 'NONE', #3502, 21.00000000000000000 ) ;
#33210=EDGE_CURVE ( 'NONE', #9886, #37732, #40608, .T. ) ;
#33234=FILL_AREA_STYLE_COLOUR ( '', #34230 ) ;
#33310=ORIENTED_EDGE ( 'NONE', *, *, #41503, .T. ) ;
#33369=AXIS2_PLACEMENT_3D ( 'NONE', #44425, #4035, #18941 ) ;
#33404=DIRECTION ( 'NONE',  ( 0.000000000000000000, 0.000000000000000000, -1.000000000000000000 ) ) ;
#33441=VERTEX_POINT ( 'NONE', #34395 ) ;
#33487=ORIENTED_EDGE ( 'NONE', *, *, #24309, .T. ) ;
#33514=PLANE ( 'NONE',  #38738 ) ;
#33542=CIRCLE ( 'NONE', #8529, 20.64000000000000057 ) ;
#33592=VECTOR ( 'NONE', #31644, 1000.000000000000000 ) ;
#33616=DIRECTION ( 'NONE',  ( 1.000000000000000000, -0.000000000000000000, -0.000000000000000000 ) ) ;
#33649=AXIS2_PLACEMENT_3D ( 'NONE', #19094, #41619, #38193 ) ;
#33693=CARTESIAN_POINT ( 'NONE',  ( -3.000000000000002665, 2.353404862842836044E-15, 19.21700905503013601 ) ) ;
#33805=EDGE_CURVE ( 'NONE', #48194, #23375, #2776, .T. ) ;
#33916=CARTESIAN_POINT ( 'NONE',  ( -10.90076147243505211, 1.679431090506078290E-15, -13.71319123027096865 ) ) ;
#33988=DIRECTION ( 'NONE',  ( -1.000000000000000000, 0.000000000000000000, 0.000000000000000000 ) ) ;
#34162=DIRECTION ( 'NONE',  ( 0.000000000000000000, 1.000000000000000000, -1.224646799147353207E-16 ) ) ;
#34230=COLOUR_RGB ( '', 0.40784314, 0.44705882, 0.49803922) ;
#34395=CARTESIAN_POINT ( 'NONE',  ( -3.759344165985237129, 2.343521743652961183E-15, 19.05560546998412974 ) ) ;
#34464=CARTESIAN_POINT ( 'NONE',  ( -0.2999999999999947153, 0.000000000000000000, 0.000000000000000000 ) ) ;
#34541=CARTESIAN_POINT ( 'NONE',  ( 6.938893903907228378E-15, 1.932465207890948911E-15, 15.77977592589476608 ) ) ;
#34578=ADVANCED_FACE ( 'NONE', ( #37433 ), #27926, .F. ) ;
#34666=VECTOR ( 'NONE', #28537, 1000.000000000000000 ) ;
#34723=CARTESIAN_POINT ( 'NONE',  ( -0.2999999999999947153, 0.000000000000000000, -12.50000000000000000 ) ) ;
#34737=CONICAL_SURFACE ( 'NONE', #23815, 15.39727592608509177, 1.361356816555577609 ) ;
#34781=FACE_OUTER_BOUND ( 'NONE', #45338, .T. ) ;
#34848=VERTEX_POINT ( 'NONE', #16606 ) ;
#34869=AXIS2_PLACEMENT_3D ( 'NONE', #35265, #27452, #16668 ) ;
#34925=ORIENTED_EDGE ( 'NONE', *, *, #768, .T. ) ;
#34935=ADVANCED_FACE ( 'NONE', ( #29318 ), #25868, .F. ) ;
#34972=CARTESIAN_POINT ( 'NONE',  ( -3.000000000000000888, 20.64000000000000057, 0.000000000000000000 ) ) ;
#34989=STYLED_ITEM ( 'NONE', ( #1510 ), #35540 ) ;
#35195=AXIS2_PLACEMENT_3D ( 'NONE', #26531, #26767, #38037 ) ;
#35212=FACE_OUTER_BOUND ( 'NONE', #12276, .T. ) ;
#35235=LINE ( 'NONE', #1237, #38787 ) ;
#35265=CARTESIAN_POINT ( 'NONE',  ( -12.00000000000000000, 0.000000000000000000, 0.000000000000000000 ) ) ;
#35509=VECTOR ( 'NONE', #47700, 1000.000000000000114 ) ;
#35540=MANIFOLD_SOLID_BREP ( 'InnerRace', #48144 ) ;
#35544=DIRECTION ( 'NONE',  ( 0.000000000000000000, 0.000000000000000000, -1.000000000000000000 ) ) ;
#35579=CYLINDRICAL_SURFACE ( 'NONE', #8794, 12.50000000000000000 ) ;
#35681=DIRECTION ( 'NONE',  ( 0.000000000000000000, 0.000000000000000000, -1.000000000000000000 ) ) ;
#35725=CARTESIAN_POINT ( 'NONE',  ( -11.68233973192911535, 0.000000000000000000, 0.000000000000000000 ) ) ;
#35755=DIRECTION ( 'NONE',  ( 0.000000000000000000, 0.000000000000000000, 1.000000000000000000 ) ) ;
#35799=COLOUR_RGB ( '', 0.40784314, 0.44705882, 0.49803922) ;
#35835=VERTEX_POINT ( 'NONE', #14121 ) ;
#35870=FACE_OUTER_BOUND ( 'NONE', #266, .T. ) ;
#35946=DIRECTION ( 'NONE',  ( 1.000000000000000000, 0.000000000000000000, 0.000000000000000000 ) ) ;
#35966=DIRECTION ( 'NONE',  ( 1.000000000000000000, 0.000000000000000000, 0.000000000000000000 ) ) ;
#36053=EDGE_LOOP ( 'NONE', ( #22894, #26702, #46363, #43066 ) ) ;
#36140=ORIENTED_EDGE ( 'NONE', *, *, #7897, .T. ) ;
#36143=DIRECTION ( 'NONE',  ( 1.000000000000000000, 0.000000000000000000, 0.000000000000000000 ) ) ;
#36148=DIRECTION ( 'NONE',  ( 1.000000000000000000, 0.000000000000000000, 0.000000000000000000 ) ) ;
#36191=AXIS2_PLACEMENT_3D ( 'NONE', #3485, #29668, #40939 ) ;
#36302=ORIENTED_EDGE ( 'NONE', *, *, #31452, .F. ) ;
#36319=CARTESIAN_POINT ( 'NONE',  ( -12.00000000000000000, 0.000000000000000000, 0.000000000000000000 ) ) ;
#36351=DIRECTION ( 'NONE',  ( -1.000000000000000000, 0.000000000000000000, -0.000000000000000000 ) ) ;
#36439=AXIS2_PLACEMENT_3D ( 'NONE', #47050, #20867, #17896 ) ;
#36451=DIRECTION ( 'NONE',  ( 0.000000000000000000, 0.000000000000000000, -1.000000000000000000 ) ) ;
#36466=ADVANCED_FACE ( 'NONE', ( #45709 ), #12468, .T. ) ;
#36517=DIRECTION ( 'NONE',  ( 1.000000000000000000, 0.000000000000000000, 0.000000000000000000 ) ) ;
#36538=ORIENTED_EDGE ( 'NONE', *, *, #4644, .F. ) ;
#36544=CARTESIAN_POINT ( 'NONE',  ( -10.90473778262209414, 0.000000000000000000, 0.000000000000000000 ) ) ;
#36549=EDGE_CURVE ( 'NONE', #20800, #22705, #47851, .T. ) ;
#36553=DIRECTION ( 'NONE',  ( 1.000000000000000000, 0.000000000000000000, 0.000000000000000000 ) ) ;
#36730=ORIENTED_EDGE ( 'NONE', *, *, #32466, .T. ) ;
#36759=CARTESIAN_POINT ( 'NONE',  ( 3.469446951953614189E-15, 12.79999999999999893, 0.000000000000000000 ) ) ;
#36784=DIRECTION ( 'NONE',  ( 0.9781476007338069101, 0.000000000000000000, -0.2079116908177528755 ) ) ;
#36842=ORIENTED_EDGE ( 'NONE', *, *, #40404, .F. ) ;
#36884=( NAMED_UNIT ( * ) PLANE_ANGLE_UNIT ( ) SI_UNIT ( $, .RADIAN. ) );
#36889=EDGE_CURVE ( 'NONE', #16167, #13391, #2235, .T. ) ;
#36899=CARTESIAN_POINT ( 'NONE',  ( -42.50000000000000000, 2.571758278209441267E-15, 20.99999999999999645 ) ) ;
#37005=AXIS2_PLACEMENT_3D ( 'NONE', #17066, #24666, #17298 ) ;
#37006=AXIS2_PLACEMENT_3D ( 'NONE', #19854, #38734, #5922 ) ;
#37045=DIRECTION ( 'NONE',  ( 1.000000000000000000, 0.000000000000000000, 0.000000000000000000 ) ) ;
#37185=DIRECTION ( 'NONE',  ( 1.000000000000000000, 0.000000000000000000, 0.000000000000000000 ) ) ;
#37250=EDGE_CURVE ( 'NONE', #19346, #35835, #31308, .T. ) ;
#37324=ORIENTED_EDGE ( 'NONE', *, *, #4644, .T. ) ;
#37343=EDGE_LOOP ( 'NONE', ( #15553, #24483, #32011, #30775 ) ) ;
#37433=FACE_OUTER_BOUND ( 'NONE', #5899, .T. ) ;
#37434=EDGE_CURVE ( 'NONE', #8908, #11885, #47449, .T. ) ;
#37447=PRODUCT_DEFINITION_CONTEXT ( 'detailed design', #29133, 'design' ) ;
#37611=AXIS2_PLACEMENT_3D ( 'NONE', #7001, #3574, #32942 ) ;
#37617=CARTESIAN_POINT ( 'NONE',  ( -11.68233973192911535, 0.000000000000000000, -17.37152077436032371 ) ) ;
#37630=DIRECTION ( 'NONE',  ( 0.000000000000000000, 0.000000000000000000, 1.000000000000000000 ) ) ;
#37655=DIRECTION ( 'NONE',  ( 0.000000000000000000, 0.000000000000000000, -1.000000000000000000 ) ) ;
#37661=ORIENTED_EDGE ( 'NONE', *, *, #5724, .F. ) ;
#37686=LINE ( 'NONE', #7341, #22921 ) ;
#37696=ORIENTED_EDGE ( 'NONE', *, *, #9839, .F. ) ;
#37732=VERTEX_POINT ( 'NONE', #46438 ) ;
#37845=DIRECTION ( 'NONE',  ( 0.000000000000000000, -1.000000000000000000, 0.000000000000000000 ) ) ;
#37875=CIRCLE ( 'NONE', #31639, 20.69999999999999929 ) ;
#37899=ORIENTED_EDGE ( 'NONE', *, *, #32466, .F. ) ;
#37954=VERTEX_POINT ( 'NONE', #3807 ) ;
#38009=DIRECTION ( 'NONE',  ( 0.000000000000000000, 0.000000000000000000, -1.000000000000000000 ) ) ;
#38012=CARTESIAN_POINT ( 'NONE',  ( -3.000000000000002665, 0.000000000000000000, 20.64000000000000057 ) ) ;
#38037=DIRECTION ( 'NONE',  ( 0.000000000000000000, 0.000000000000000000, -1.000000000000000000 ) ) ;
#38146=DIRECTION ( 'NONE',  ( 1.000000000000000000, 0.000000000000000000, 0.000000000000000000 ) ) ;
#38155=EDGE_LOOP ( 'NONE', ( #40895, #33310 ) ) ;
#38156=DIRECTION ( 'NONE',  ( 0.000000000000000000, 0.000000000000000000, -1.000000000000000000 ) ) ;
#38157=DIRECTION ( 'NONE',  ( 0.000000000000000000, 0.000000000000000000, -1.000000000000000000 ) ) ;
#38193=DIRECTION ( 'NONE',  ( 0.000000000000000000, 0.000000000000000000, 1.000000000000000000 ) ) ;
#38220=CIRCLE ( 'NONE', #714, 12.50000000000000000 ) ;
#38269=DIRECTION ( 'NONE',  ( 0.000000000000000000, 0.000000000000000000, -1.000000000000000000 ) ) ;
#38304=EDGE_CURVE ( 'NONE', #1706, #9886, #3890, .T. ) ;
#38359=CIRCLE ( 'NONE', #31319, 12.85999999999999943 ) ;
#38395=DIRECTION ( 'NONE',  ( 0.000000000000000000, 0.000000000000000000, 1.000000000000000000 ) ) ;
#38415=CIRCLE ( 'NONE', #25123, 15.39727592589476579 ) ;
#38461=CARTESIAN_POINT ( 'NONE',  ( -10.90076147243505211, 0.000000000000000000, 0.000000000000000000 ) ) ;
#38578=CONICAL_SURFACE ( 'NONE', #22141, 17.30399999999999849, 0.2094395102393129815 ) ;
#38619=CARTESIAN_POINT ( 'NONE',  ( -11.69999999999999929, 0.000000000000000000, -20.99999999999999645 ) ) ;
#38634=AXIS2_PLACEMENT_3D ( 'NONE', #18808, #41834, #41115 ) ;
#38730=TOROIDAL_SURFACE ( 'NONE', #6675, 20.69999999999999929, 0.2999999999999981570 ) ;
#38734=DIRECTION ( 'NONE',  ( 1.000000000000000000, 0.000000000000000000, 0.000000000000000000 ) ) ;
#38738=AXIS2_PLACEMENT_3D ( 'NONE', #7086, #11505, #26431 ) ;
#38765=VERTEX_POINT ( 'NONE', #13272 ) ;
#38787=VECTOR ( 'NONE', #12984, 1000.000000000000000 ) ;
#38915=VERTEX_POINT ( 'NONE', #11477 ) ;
#38951=DIRECTION ( 'NONE',  ( 1.000000000000000000, 0.000000000000000000, 0.000000000000000000 ) ) ;
#38989=CARTESIAN_POINT ( 'NONE',  ( -11.99999999999999645, 0.000000000000000000, -20.69999999999999929 ) ) ;
#38992=CARTESIAN_POINT ( 'NONE',  ( -2.977765906491215642, 0.000000000000000000, 0.000000000000000000 ) ) ;
#39076=ADVANCED_FACE ( 'NONE', ( #33196 ), #2404, .T. ) ;
#39103=ORIENTED_EDGE ( 'NONE', *, *, #13668, .T. ) ;
#39185=FACE_OUTER_BOUND ( 'NONE', #3031, .T. ) ;
#39269=AXIS2_PLACEMENT_3D ( 'NONE', #42072, #33988, #38395 ) ;
#39279=EDGE_LOOP ( 'NONE', ( #37324, #10851, #9848, #44727 ) ) ;
#39377=FACE_OUTER_BOUND ( 'NONE', #12747, .T. ) ;
#39570=DIRECTION ( 'NONE',  ( 0.000000000000000000, 0.000000000000000000, 1.000000000000000000 ) ) ;
#39663=AXIS2_PLACEMENT_3D ( 'NONE', #15174, #30099, #45027 ) ;
#39667=CARTESIAN_POINT ( 'NONE',  ( -2.977765906491215642, 0.000000000000000000, 0.000000000000000000 ) ) ;
#39668=ORIENTED_EDGE ( 'NONE', *, *, #5724, .T. ) ;
#39795=ADVANCED_FACE ( 'NONE', ( #27495 ), #32206, .F. ) ;
#39797=CARTESIAN_POINT ( 'NONE',  ( -11.99999999999999645, 0.000000000000000000, 12.85999999999999943 ) ) ;
#39823=AXIS2_PLACEMENT_3D ( 'NONE', #43001, #20725, #17043 ) ;
#39830=CARTESIAN_POINT ( 'NONE',  ( -2.977765906491215642, 0.000000000000000000, 0.000000000000000000 ) ) ;
#39889=DIRECTION ( 'NONE',  ( 0.000000000000000000, 0.000000000000000000, -1.000000000000000000 ) ) ;
#39965=LINE ( 'NONE', #28457, #26617 ) ;
#40038=DIRECTION ( 'NONE',  ( -1.000000000000000000, -0.000000000000000000, -0.000000000000000000 ) ) ;
#40102=VECTOR ( 'NONE', #8298, 1000.000000000000227 ) ;
#40163=ADVANCED_FACE ( 'NONE', ( #25047 ), #38578, .F. ) ;
#40166=CIRCLE ( 'NONE', #7342, 20.99999999999999645 ) ;
#40256=EDGE_CURVE ( 'NONE', #38765, #37954, #29458, .T. ) ;
#40346=CONICAL_SURFACE ( 'NONE', #34869, 17.30399999999999849, 0.2094395102393129815 ) ;
#40347=EDGE_CURVE ( 'NONE', #22027, #38915, #22986, .T. ) ;
#40388=EDGE_LOOP ( 'NONE', ( #30645, #26449, #6082, #18003 ) ) ;
#40404=EDGE_CURVE ( 'NONE', #44810, #11885, #41679, .T. ) ;
#40424=ADVANCED_FACE ( 'NONE', ( #28191 ), #16701, .T. ) ;
#40608=LINE ( 'NONE', #47697, #18361 ) ;
#40775=ADVANCED_FACE ( 'NONE', ( #15204 ), #29744, .F. ) ;
#40809=CARTESIAN_POINT ( 'NONE',  ( -42.50000000000000000, 0.000000000000000000, 0.000000000000000000 ) ) ;
#40895=ORIENTED_EDGE ( 'NONE', *, *, #12643, .T. ) ;
#40923=ORIENTED_EDGE ( 'NONE', *, *, #40256, .T. ) ;
#40939=DIRECTION ( 'NONE',  ( 0.000000000000000000, 0.000000000000000000, -1.000000000000000000 ) ) ;
#41013=CARTESIAN_POINT ( 'NONE',  ( -10.94538922500103162, 0.000000000000000000, 13.90444123027096879 ) ) ;
#41053=CARTESIAN_POINT ( 'NONE',  ( -0.2999999999999964362, 0.000000000000000000, -12.80000000000000071 ) ) ;
#41115=DIRECTION ( 'NONE',  ( 0.000000000000000000, 0.000000000000000000, 1.000000000000000000 ) ) ;
#41197=EDGE_LOOP ( 'NONE', ( #27769, #28438 ) ) ;
#41314=EDGE_CURVE ( 'NONE', #8938, #14976, #23933, .T. ) ;
#41476=EDGE_CURVE ( 'NONE', #3678, #38915, #46928, .T. ) ;
#41481=DIRECTION ( 'NONE',  ( 1.000000000000000000, 0.000000000000000000, 0.000000000000000000 ) ) ;
#41502=DIRECTION ( 'NONE',  ( 1.000000000000000000, 0.000000000000000000, 0.000000000000000000 ) ) ;
#41503=EDGE_CURVE ( 'NONE', #22671, #30256, #38415, .T. ) ;
#41516=ORIENTED_EDGE ( 'NONE', *, *, #23951, .F. ) ;
#41598=DIRECTION ( 'NONE',  ( 0.000000000000000000, 0.000000000000000000, -1.000000000000000000 ) ) ;
#41619=DIRECTION ( 'NONE',  ( -1.000000000000000000, -0.000000000000000000, -0.000000000000000000 ) ) ;
#41679=LINE ( 'NONE', #38012, #2632 ) ;
#41698=CARTESIAN_POINT ( 'NONE',  ( -11.99999999999999645, 0.000000000000000000, 12.85999999999999943 ) ) ;
#41762=DIRECTION ( 'NONE',  ( 0.000000000000000000, 0.000000000000000000, -1.000000000000000000 ) ) ;
#41831=ORIENTED_EDGE ( 'NONE', *, *, #21139, .F. ) ;
#41834=DIRECTION ( 'NONE',  ( -1.000000000000000000, -0.000000000000000000, -0.000000000000000000 ) ) ;
#41881=ORIENTED_EDGE ( 'NONE', *, *, #25012, .T. ) ;
#42009=CARTESIAN_POINT ( 'NONE',  ( -11.69999999999999929, 0.000000000000000000, 0.000000000000000000 ) ) ;
#42072=CARTESIAN_POINT ( 'NONE',  ( -10.94538922500103162, 0.000000000000000000, 0.000000000000000000 ) ) ;
#42265=ORIENTED_EDGE ( 'NONE', *, *, #1957, .F. ) ;
#42326=VECTOR ( 'NONE', #31285, 1000.000000000000000 ) ;
#42425=DIRECTION ( 'NONE',  ( 0.000000000000000000, 0.000000000000000000, 1.000000000000000000 ) ) ;
#42488=DIRECTION ( 'NONE',  ( 1.000000000000000000, 0.000000000000000000, 0.000000000000000000 ) ) ;
#42593=VECTOR ( 'NONE', #45077, 1000.000000000000114 ) ;
#42637=SURFACE_STYLE_USAGE ( .BOTH. , #19849 ) ;
#42825=ORIENTED_EDGE ( 'NONE', *, *, #36889, .T. ) ;
#42830=EDGE_CURVE ( 'NONE', #35835, #30318, #44026, .T. ) ;
#42860=CARTESIAN_POINT ( 'NONE',  ( -11.99999999999999645, 0.000000000000000000, 0.000000000000000000 ) ) ;
#42946=( GEOMETRIC_REPRESENTATION_CONTEXT ( 3 ) GLOBAL_UNCERTAINTY_ASSIGNED_CONTEXT ( ( #26677 ) ) GLOBAL_UNIT_ASSIGNED_CONTEXT ( ( #2630, #36884, #3611 ) ) REPRESENTATION_CONTEXT ( 'NONE', 'WORKASPACE' ) );
#43001=CARTESIAN_POINT ( 'NONE',  ( -0.2999999999999964362, 0.000000000000000000, 0.000000000000000000 ) ) ;
#43016=EDGE_LOOP ( 'NONE', ( #2697, #23363, #42825, #804 ) ) ;
#43066=ORIENTED_EDGE ( 'NONE', *, *, #23097, .F. ) ;
#43153=CARTESIAN_POINT ( 'NONE',  ( -10.90473778262209414, 0.000000000000000000, 0.000000000000000000 ) ) ;
#43274=VECTOR ( 'NONE', #27874, 1000.000000000000000 ) ;
#43283=ADVANCED_FACE ( 'NONE', ( #8889 ), #27652, .F. ) ;
#43478=ORIENTED_EDGE ( 'NONE', *, *, #44319, .F. ) ;
#43538=ORIENTED_EDGE ( 'NONE', *, *, #1704, .T. ) ;
#43556=DIRECTION ( 'NONE',  ( -1.000000000000000000, 0.000000000000000000, 0.000000000000000000 ) ) ;
#43596=ADVANCED_FACE ( 'NONE', ( #4143 ), #11268, .F. ) ;
#43617=EDGE_CURVE ( 'NONE', #27937, #46875, #30032, .T. ) ;
#43643=DIRECTION ( 'NONE',  ( 1.000000000000000000, 0.000000000000000000, 0.000000000000000000 ) ) ;
#43668=DIRECTION ( 'NONE',  ( 0.000000000000000000, 0.000000000000000000, -1.000000000000000000 ) ) ;
#43710=EDGE_LOOP ( 'NONE', ( #31599, #37661 ) ) ;
#43716=ORIENTED_EDGE ( 'NONE', *, *, #38304, .F. ) ;
#43782=ORIENTED_EDGE ( 'NONE', *, *, #9945, .T. ) ;
#43813=CARTESIAN_POINT ( 'NONE',  ( -11.99999999999999645, 0.000000000000000000, -13.90444123027096879 ) ) ;
#43917=FACE_OUTER_BOUND ( 'NONE', #1617, .T. ) ;
#43930=EDGE_LOOP ( 'NONE', ( #29833, #6366, #3469, #6057 ) ) ;
#43934=AXIS2_PLACEMENT_3D ( 'NONE', #2807, #47590, #28991 ) ;
#43968=CARTESIAN_POINT ( 'NONE',  ( -12.00000000000000000, 2.119128821244579932E-15, 17.30399999999999849 ) ) ;
#44026=CIRCLE ( 'NONE', #28376, 0.2999999999999999334 ) ;
#44085=CARTESIAN_POINT ( 'NONE',  ( -3.000000000000002665, 0.000000000000000000, 0.000000000000000000 ) ) ;
#44191=CIRCLE ( 'NONE', #9838, 15.39727592608509177 ) ;
#44319=EDGE_CURVE ( 'NONE', #8938, #29208, #19895, .T. ) ;
#44354=CARTESIAN_POINT ( 'NONE',  ( -3.000000000000002665, 0.000000000000000000, 0.000000000000000000 ) ) ;
#44425=CARTESIAN_POINT ( 'NONE',  ( -42.50000000000000000, 0.000000000000000000, 0.000000000000000000 ) ) ;
#44471=ORIENTED_EDGE ( 'NONE', *, *, #27739, .T. ) ;
#44505=VERTEX_POINT ( 'NONE', #24299 ) ;
#44540=ORIENTED_EDGE ( 'NONE', *, *, #12827, .T. ) ;
#44557=EDGE_LOOP ( 'NONE', ( #36302, #31471, #40923, #9225 ) ) ;
#44590=CARTESIAN_POINT ( 'NONE',  ( -11.63999999999999702, 1.552852141318844077E-15, -12.50000000000000000 ) ) ;
#44627=CONICAL_SURFACE ( 'NONE', #21949, 13.71319123046128752, 0.2094395102393127317 ) ;
#44697=CARTESIAN_POINT ( 'NONE',  ( -11.70000000000000107, 2.535018874235021196E-15, 20.69999999999999929 ) ) ;
#44727=ORIENTED_EDGE ( 'NONE', *, *, #26489, .F. ) ;
#44810=VERTEX_POINT ( 'NONE', #46046 ) ;
#44840=AXIS2_PLACEMENT_3D ( 'NONE', #10450, #36148, #2604 ) ;
#44853=AXIS2_PLACEMENT_3D ( 'NONE', #42860, #38951, #27206 ) ;
#44875=CARTESIAN_POINT ( 'NONE',  ( -11.63999999999999702, 0.000000000000000000, 12.50000000000000000 ) ) ;
#44944=ORIENTED_EDGE ( 'NONE', *, *, #14156, .F. ) ;
#45027=DIRECTION ( 'NONE',  ( 0.000000000000000000, 0.000000000000000000, -1.000000000000000000 ) ) ;
#45048=EDGE_CURVE ( 'NONE', #28565, #28374, #2437, .T. ) ;
#45077=DIRECTION ( 'NONE',  ( -0.2079116908177587875, 1.197885328332318196E-16, -0.9781476007338056888 ) ) ;
#45123=CARTESIAN_POINT ( 'NONE',  ( -0.2999999999999947153, 0.000000000000000000, 0.000000000000000000 ) ) ;
#45162=EDGE_CURVE ( 'NONE', #13391, #11885, #33197, .T. ) ;
#45338=EDGE_LOOP ( 'NONE', ( #2391, #43716, #24026, #17757 ) ) ;
#45553=EDGE_LOOP ( 'NONE', ( #31212, #777, #16877, #3275 ) ) ;
#45556=FILL_AREA_STYLE_COLOUR ( '', #35799 ) ;
#45557=CONICAL_SURFACE ( 'NONE', #46339, 13.71319123046128752, 0.2094395102393127317 ) ;
#45592=TOROIDAL_SURFACE ( 'NONE', #24501, 20.69999999999999929, 0.2999999999999981570 ) ;
#45709=FACE_OUTER_BOUND ( 'NONE', #32519, .T. ) ;
#45947=AXIS2_PLACEMENT_3D ( 'NONE', #40809, #48388, #7269 ) ;
#45968=ADVANCED_FACE ( 'NONE', ( #34781 ), #23914, .T. ) ;
#46046=CARTESIAN_POINT ( 'NONE',  ( -3.000000000000002665, 0.000000000000000000, 20.64000000000000057 ) ) ;
#46089=CARTESIAN_POINT ( 'NONE',  ( -3.759344165985237129, 0.000000000000000000, 0.000000000000000000 ) ) ;
#46140=ADVANCED_FACE ( 'NONE', ( #39185 ), #40346, .F. ) ;
#46153=CARTESIAN_POINT ( 'NONE',  ( -11.69999999999999929, 0.000000000000000000, 0.000000000000000000 ) ) ;
#46235=CARTESIAN_POINT ( 'NONE',  ( -2.977765906491215642, 0.000000000000000000, -15.39727592589476579 ) ) ;
#46328=DIRECTION ( 'NONE',  ( 0.000000000000000000, 0.000000000000000000, -1.000000000000000000 ) ) ;
#46339=AXIS2_PLACEMENT_3D ( 'NONE', #36544, #47552, #17930 ) ;
#46363=ORIENTED_EDGE ( 'NONE', *, *, #9048, .T. ) ;
#46429=AXIS2_PLACEMENT_3D ( 'NONE', #12075, #11581, #38009 ) ;
#46438=CARTESIAN_POINT ( 'NONE',  ( -10.90093335751250692, 0.000000000000000000, -13.71399988598171049 ) ) ;
#46594=ORIENTED_EDGE ( 'NONE', *, *, #9513, .F. ) ;
#46611=AXIS2_PLACEMENT_3D ( 'NONE', #20486, #36143, #21206 ) ;
#46651=LINE ( 'NONE', #13351, #33026 ) ;
#46678=CONICAL_SURFACE ( 'NONE', #2123, 15.39727592589476579, 0.2094395102393128150 ) ;
#46755=DIRECTION ( 'NONE',  ( 0.000000000000000000, 0.000000000000000000, 1.000000000000000000 ) ) ;
#46875=VERTEX_POINT ( 'NONE', #12894 ) ;
#46893=AXIS2_PLACEMENT_3D ( 'NONE', #26759, #1041, #8399 ) ;
#46928=LINE ( 'NONE', #43968, #28244 ) ;
#46938=EDGE_LOOP ( 'NONE', ( #39103, #5746, #29802, #33117 ) ) ;
#46943=ORIENTED_EDGE ( 'NONE', *, *, #7822, .F. ) ;
#46979=EDGE_LOOP ( 'NONE', ( #18298, #15311, #27655, #31606 ) ) ;
#47050=CARTESIAN_POINT ( 'NONE',  ( -11.99999999999999645, 0.000000000000000000, 0.000000000000000000 ) ) ;
#47084=CIRCLE ( 'NONE', #43934, 20.64000000000000057 ) ;
#47126=CARTESIAN_POINT ( 'NONE',  ( -42.50000000000000000, 1.932465207890948911E-15, 15.77977592589476608 ) ) ;
#47171=CYLINDRICAL_SURFACE ( 'NONE', #37005, 15.77977592589476608 ) ;
#47176=ADVANCED_FACE ( 'NONE', ( #24855 ), #27165, .T. ) ;
#47276=ADVANCED_FACE ( 'NONE', ( #19423 ), #3547, .T. ) ;
#47294=DIRECTION ( 'NONE',  ( 0.000000000000000000, 0.000000000000000000, 1.000000000000000000 ) ) ;
#47366=DIRECTION ( 'NONE',  ( 0.000000000000000000, 0.000000000000000000, -1.000000000000000000 ) ) ;
#47449=LINE ( 'NONE', #36899, #21039 ) ;
#47552=DIRECTION ( 'NONE',  ( 1.000000000000000000, -0.000000000000000000, -0.000000000000000000 ) ) ;
#47590=DIRECTION ( 'NONE',  ( 1.000000000000000000, 0.000000000000000000, 0.000000000000000000 ) ) ;
#47596=VECTOR ( 'NONE', #25105, 1000.000000000000227 ) ;
#47664=CONICAL_SURFACE ( 'NONE', #26581, 15.39727592589476579, 0.2094395102393128150 ) ;
#47697=CARTESIAN_POINT ( 'NONE',  ( -10.90076147243505211, 1.679381574624689562E-15, -13.71319123027096865 ) ) ;
#47699=EDGE_LOOP ( 'NONE', ( #16211, #43538 ) ) ;
#47700=DIRECTION ( 'NONE',  ( -0.7071067811865474617, 8.659560562354932858E-17, -0.7071067811865474617 ) ) ;
#47726=ADVANCED_FACE ( 'NONE', ( #26672 ), #23308, .T. ) ;
#47792=AXIS2_PLACEMENT_3D ( 'NONE', #27737, #16238, #12799 ) ;
#47851=LINE ( 'NONE', #2347, #47596 ) ;
#47905=PRESENTATION_STYLE_ASSIGNMENT (( #25875 ) ) ;
#47970=DIRECTION ( 'NONE',  ( 0.9781476007338069101, 2.546183866652752180E-17, 0.2079116908177528755 ) ) ;
#48011=CARTESIAN_POINT ( 'NONE',  ( -3.000000000000002665, 0.000000000000000000, 0.000000000000000000 ) ) ;
#48067=CARTESIAN_POINT ( 'NONE',  ( -10.90076147243505211, 0.000000000000000000, 13.71319123027096865 ) ) ;
#48073=ORIENTED_EDGE ( 'NONE', *, *, #5597, .T. ) ;
#48144=CLOSED_SHELL ( 'NONE', ( #18446, #9490, #36466, #29644, #43596, #47276, #47726, #39076, #5384, #3624, #17283, #18283, #32338, #34578, #39795, #46140, #30280, #40163, #10723, #30348, #40424, #47176, #43283, #30857, #23169, #45968, #19600, #7226, #40775, #34935, #15912, #3054, #4646, #29116, #2730 ) ) ;
#48194=VERTEX_POINT ( 'NONE', #23777 ) ;
#48214=CONICAL_SURFACE ( 'NONE', #27124, 17.45460580326810174, 1.361356816555583826 ) ;
#48325=CARTESIAN_POINT ( 'NONE',  ( -2.977765906491215642, 0.000000000000000000, 0.000000000000000000 ) ) ;
#48388=DIRECTION ( 'NONE',  ( 1.000000000000000000, 0.000000000000000000, 0.000000000000000000 ) ) ;
ENDSEC;
END-ISO-10303-21;
